ISO-10303-21;
HEADER;
FILE_DESCRIPTION (('STEP AP214'),
    '1' );
FILE_NAME ('hex thin nut chamfered gradeab_iso_ISO - 4035 - M5 - N.step',
    '2026-10-08T12:12:07',
    ( '' ),
    ( '' ),
    'SwSTEP 2.0',
    'SolidWorks 2026',
    '' );
FILE_SCHEMA (( 'AUTOMOTIVE_DESIGN' ));
ENDSEC;

DATA;
#12=B_SPLINE_CURVE_WITH_KNOTS ( 'NONE', 3,
 ( #534, #1149, #5570, #2945, #3074, #6720 ),
 .UNSPECIFIED., .F., .F.,
 ( 4, 2, 4 ),
 ( 0.006456566858647395761, 0.007625406818786665576, 0.008794246778925936259 ),
 .UNSPECIFIED. ) ;
#20=DIRECTION ( 'NONE',  ( 0.8191520442889896891, 1.003171929053522158E-16, -0.5735764363510490460 ) ) ;
#25=CARTESIAN_POINT ( 'NONE',  ( 0.000000000000000000, 0.000000000000000000, 0.000000000000000000 ) ) ;
#38=ORIENTED_EDGE ( 'NONE', *, *, #3972, .T. ) ;
#61=DIRECTION ( 'NONE',  ( -1.000000000000000000, 0.000000000000000000, 0.000000000000000000 ) ) ;
#63=EDGE_CURVE ( 'NONE', #397, #8121, #700, .T. ) ;
#70=( NAMED_UNIT ( * ) SI_UNIT ( $, .STERADIAN. ) SOLID_ANGLE_UNIT ( ) );
#80=DIRECTION ( 'NONE',  ( 0.000000000000000000, -0.000000000000000000, 1.000000000000000000 ) ) ;
#83=ORIENTED_EDGE ( 'NONE', *, *, #3647, .F. ) ;
#110=FACE_BOUND ( 'NONE', #6288, .T. ) ;
#115=CARTESIAN_POINT ( 'NONE',  ( 2.339468227445713477, 3.268109542640642573, 2.462324777668250297E-15 ) ) ;
#121=CARTESIAN_POINT ( 'NONE',  ( -2.500000000000002220, 3.061616997868386099E-16, -2.700000000000001066 ) ) ;
#131=B_SPLINE_CURVE_WITH_KNOTS ( 'NONE', 3,
 ( #1454, #3993, #5161, #1526 ),
 .UNSPECIFIED., .F., .F.,
 ( 4, 4 ),
 ( 2.380737581622003645E-07, 0.002336974151641576375 ),
 .UNSPECIFIED. ) ;
#153=CARTESIAN_POINT ( 'NONE',  ( -0.6543461111163947352, -4.241015250120822699, -2.560849780464845793 ) ) ;
#164=PLANE ( 'NONE',  #4502 ) ;
#175=CARTESIAN_POINT ( 'NONE',  ( -2.000000000000009770, 3.464101615137749057, 0.000000000000000000 ) ) ;
#187=EDGE_CURVE ( 'NONE', #4246, #4613, #12, .T. ) ;
#195=CARTESIAN_POINT ( 'NONE',  ( -2.060000000000000941, 2.522772406243548923E-16, -0.3080913168122707546 ) ) ;
#210=DIRECTION ( 'NONE',  ( -1.000000000000000000, 0.000000000000000000, 0.000000000000000000 ) ) ;
#217=CARTESIAN_POINT ( 'NONE',  ( 4.000000000000000000, 0.000000000000000000, -2.700000000000001066 ) ) ;
#218=DIRECTION ( 'NONE',  ( 1.000000000000000000, 0.000000000000000000, 0.000000000000000000 ) ) ;
#220=EDGE_CURVE ( 'NONE', #3553, #6469, #2177, .T. ) ;
#221=CARTESIAN_POINT ( 'NONE',  ( 2.678494666091051801, 3.072372537026354156, -0.03421028094653037754 ) ) ;
#226=PLANE ( 'NONE',  #6849 ) ;
#227=PRODUCT_DEFINITION_CONTEXT ( 'detailed design', #7630, 'design' ) ;
#248=CONICAL_SURFACE ( 'NONE', #3450, 4.000000000000000000, 1.047197551196595855 ) ;
#251=PLANE ( 'NONE',  #1285 ) ;
#275=CARTESIAN_POINT ( 'NONE',  ( 4.000000000000003553, 1.935983797701078757, -2.450530693383765612 ) ) ;
#287=DIRECTION ( 'NONE',  ( 1.000000000000000000, 0.000000000000000000, 0.000000000000000000 ) ) ;
#300=ORIENTED_EDGE ( 'NONE', *, *, #63, .T. ) ;
#309=EDGE_CURVE ( 'NONE', #5533, #6468, #2599, .T. ) ;
#318=CARTESIAN_POINT ( 'NONE',  ( 3.999999999999989786, -2.309401076758547777, -2.342734410091827701 ) ) ;
#333=FACE_OUTER_BOUND ( 'NONE', #4314, .T. ) ;
#334=AXIS2_PLACEMENT_3D ( 'NONE', #7679, #2694, #3873 ) ;
#340=EDGE_LOOP ( 'NONE', ( #4876, #7853, #1305 ) ) ;
#343=CARTESIAN_POINT ( 'NONE',  ( 1.084202172485504434E-14, 4.618802153517020948, -2.342734410091827701 ) ) ;
#348=CARTESIAN_POINT ( 'NONE',  ( -4.000000000000000000, 2.309401076758496263, -2.700000000000000178 ) ) ;
#349=ORIENTED_EDGE ( 'NONE', *, *, #6360, .F. ) ;
#362=CIRCLE ( 'NONE', #5165, 4.000000000000000888 ) ;
#365=ORIENTED_EDGE ( 'NONE', *, *, #220, .T. ) ;
#366=VERTEX_POINT ( 'NONE', #4564 ) ;
#375=DIRECTION ( 'NONE',  ( 0.8660254037844352659, -0.5000000000000056621, 0.000000000000000000 ) ) ;
#391=DIRECTION ( 'NONE',  ( -0.000000000000000000, -0.000000000000000000, 1.000000000000000000 ) ) ;
#395=CONICAL_SURFACE ( 'NONE', #3069, 2.500000000000002220, 0.9599310885968777018 ) ;
#396=DIRECTION ( 'NONE',  ( 0.000000000000000000, 0.000000000000000000, 1.000000000000000000 ) ) ;
#397=VERTEX_POINT ( 'NONE', #3159 ) ;
#414=DIRECTION ( 'NONE',  ( -0.000000000000000000, 0.000000000000000000, -1.000000000000000000 ) ) ;
#424=CARTESIAN_POINT ( 'NONE',  ( -2.500000000000002220, 0.000000000000000000, -2.674599999999998978 ) ) ;
#429=ORIENTED_EDGE ( 'NONE', *, *, #1667, .F. ) ;
#432=CARTESIAN_POINT ( 'NONE',  ( -3.344563996438217224, -2.687817229851499068, -0.1586754815285014442 ) ) ;
#443=B_SPLINE_CURVE_WITH_KNOTS ( 'NONE', 3,
 ( #7017, #115, #221, #1456, #735, #4569 ),
 .UNSPECIFIED., .F., .F.,
 ( 4, 2, 4 ),
 ( 0.002336974151641576375, 0.003500975885716453226, 0.004664977619791330077 ),
 .UNSPECIFIED. ) ;
#444=CARTESIAN_POINT ( 'NONE',  ( -7.502679033599690683E-14, -4.618802153517020059, -0.3572655899081733644 ) ) ;
#464=ADVANCED_FACE ( 'NONE', ( #7171 ), #7293, .T. ) ;
#476=DIRECTION ( 'NONE',  ( -0.000000000000000000, -0.000000000000000000, 1.000000000000000000 ) ) ;
#488=CARTESIAN_POINT ( 'NONE',  ( 3.345653888883671545, -2.687187980154741140, -0.1391502195351559668 ) ) ;
#505=EDGE_CURVE ( 'NONE', #4602, #5524, #983, .T. ) ;
#534=CARTESIAN_POINT ( 'NONE',  ( -4.000000000000000000, 0.000000000000000000, -2.700000000000000178 ) ) ;
#535=CARTESIAN_POINT ( 'NONE',  ( 3.999999999999989786, -2.309401076758547777, -2.342734410091827701 ) ) ;
#564=ORIENTED_EDGE ( 'NONE', *, *, #5523, .T. ) ;
#573=ORIENTED_EDGE ( 'NONE', *, *, #2075, .F. ) ;
#647=ORIENTED_EDGE ( 'NONE', *, *, #7062, .F. ) ;
#683=VERTEX_POINT ( 'NONE', #121 ) ;
#689=ORIENTED_EDGE ( 'NONE', *, *, #2432, .F. ) ;
#700=B_SPLINE_CURVE_WITH_KNOTS ( 'NONE', 3,
 ( #7879, #7842, #823, #986, #6552, #4728 ),
 .UNSPECIFIED., .F., .F.,
 ( 4, 2, 4 ),
 ( 0.002336974151641522165, 0.003500975885716454527, 0.004664977619791387323 ),
 .UNSPECIFIED. ) ;
#701=CARTESIAN_POINT ( 'NONE',  ( -2.000000000000009770, 3.464101615137749057, -2.700000000000001066 ) ) ;
#735=CARTESIAN_POINT ( 'NONE',  ( 3.673643420401901505, 2.497823135841253706, -0.2484800633749944254 ) ) ;
#740=ORIENTED_EDGE ( 'NONE', *, *, #1500, .F. ) ;
#752=EDGE_CURVE ( 'NONE', #6523, #4246, #5461, .T. ) ;
#754=EDGE_CURVE ( 'NONE', #1392, #855, #2776, .T. ) ;
#771=CONICAL_SURFACE ( 'NONE', #7073, 4.000000000000000000, 1.047197551196595855 ) ;
#774=FILL_AREA_STYLE_COLOUR ( '', #7699 ) ;
#781=AXIS2_PLACEMENT_3D ( 'NONE', #7408, #5510, #7497 ) ;
#782=ORIENTED_EDGE ( 'NONE', *, *, #6360, .T. ) ;
#785=ORIENTED_EDGE ( 'NONE', *, *, #754, .F. ) ;
#810=ADVANCED_FACE ( 'NONE', ( #1825 ), #1191, .T. ) ;
#823=CARTESIAN_POINT ( 'NONE',  ( 1.321505333908969293, -3.855830693249187480, -2.665789719053444529 ) ) ;
#825=LINE ( 'NONE', #195, #3567 ) ;
#850=CARTESIAN_POINT ( 'NONE',  ( 0.000000000000000000, 0.000000000000000000, -2.700000000000000178 ) ) ;
#855=VERTEX_POINT ( 'NONE', #1019 ) ;
#860=EDGE_CURVE ( 'NONE', #6726, #3614, #3562, .T. ) ;
#902=DIRECTION ( 'NONE',  ( -1.000000000000000000, 0.000000000000000000, 0.000000000000000000 ) ) ;
#907=AXIS2_PLACEMENT_3D ( 'NONE', #7373, #1691, #936 ) ;
#922=ADVANCED_FACE ( 'NONE', ( #7467 ), #3045, .F. ) ;
#936=DIRECTION ( 'NONE',  ( 1.000000000000000000, 0.000000000000000000, 0.000000000000000000 ) ) ;
#950=CARTESIAN_POINT ( 'NONE',  ( -2.099999999999999645, 2.571758278209440478E-16, -2.700000000000000178 ) ) ;
#964=ADVANCED_FACE ( 'NONE', ( #7715 ), #395, .F. ) ;
#969=CARTESIAN_POINT ( 'NONE',  ( -7.502679033599690683E-14, -4.618802153517020059, -0.3572655899081733644 ) ) ;
#970=DIRECTION ( 'NONE',  ( -0.000000000000000000, -0.000000000000000000, 1.000000000000000000 ) ) ;
#983=CIRCLE ( 'NONE', #3122, 2.099999999999999645 ) ;
#986=CARTESIAN_POINT ( 'NONE',  ( 0.6554360035617803337, -4.240386000424090085, -2.541324518471480332 ) ) ;
#995=DIRECTION ( 'NONE',  ( 1.000000000000000000, 0.000000000000000000, 0.000000000000000000 ) ) ;
#1000=DIRECTION ( 'NONE',  ( 0.000000000000000000, 0.000000000000000000, 1.000000000000000000 ) ) ;
#1005=FACE_OUTER_BOUND ( 'NONE', #340, .T. ) ;
#1019=CARTESIAN_POINT ( 'NONE',  ( 2.500000000000000444, 0.000000000000000000, 3.469446951953614189E-15 ) ) ;
#1033=CONICAL_SURFACE ( 'NONE', #2227, 4.000000000000000000, 1.047197551196595855 ) ;
#1047=CARTESIAN_POINT ( 'NONE',  ( 4.000000000000002665, 1.935983797701077869, -0.2494693066162346762 ) ) ;
#1063=CARTESIAN_POINT ( 'NONE',  ( -2.678494666091066012, -3.072372537026387018, -0.03421028094655010482 ) ) ;
#1069=DIRECTION ( 'NONE',  ( 0.000000000000000000, 0.000000000000000000, -1.000000000000000000 ) ) ;
#1075=CARTESIAN_POINT ( 'NONE',  ( -7.502679033599690683E-14, -4.618802153517020059, -0.3572655899081733644 ) ) ;
#1115=CARTESIAN_POINT ( 'NONE',  ( -4.000000000000000000, -1.933795701539609668, -0.2488376576622978453 ) ) ;
#1122=EDGE_LOOP ( 'NONE', ( #573, #785 ) ) ;
#1128=EDGE_CURVE ( 'NONE', #6469, #3165, #5928, .T. ) ;
#1149=CARTESIAN_POINT ( 'NONE',  ( -4.000000000000000000, 0.3904826640788065517, -2.700000000000001510 ) ) ;
#1151=CARTESIAN_POINT ( 'NONE',  ( -2.099999999999999645, 2.571758278209440478E-16, -2.394516984716111185 ) ) ;
#1160=AXIS2_PLACEMENT_3D ( 'NONE', #6041, #2890, #5432 ) ;
#1168=FILL_AREA_STYLE ('',( #6910 ) ) ;
#1184=EDGE_CURVE ( 'NONE', #4714, #5524, #2806, .T. ) ;
#1191=CONICAL_SURFACE ( 'NONE', #5709, 4.000000000000000000, 1.047197551196595855 ) ;
#1199=DIRECTION ( 'NONE',  ( 0.000000000000000000, 0.000000000000000000, -1.000000000000000000 ) ) ;
#1244=ORIENTED_EDGE ( 'NONE', *, *, #2547, .T. ) ;
#1254=ORIENTED_EDGE ( 'NONE', *, *, #3053, .F. ) ;
#1258=VERTEX_POINT ( 'NONE', #4935 ) ;
#1260=DIRECTION ( 'NONE',  ( 0.000000000000000000, 0.000000000000000000, 1.000000000000000000 ) ) ;
#1273=FACE_OUTER_BOUND ( 'NONE', #5568, .T. ) ;
#1281=DIRECTION ( 'NONE',  ( 0.000000000000000000, 0.000000000000000000, 1.000000000000000000 ) ) ;
#1285=AXIS2_PLACEMENT_3D ( 'NONE', #6028, #4968, #375 ) ;
#1286=ORIENTED_EDGE ( 'NONE', *, *, #5596, .T. ) ;
#1305=ORIENTED_EDGE ( 'NONE', *, *, #6099, .F. ) ;
#1306=AXIS2_PLACEMENT_3D ( 'NONE', #2270, #5477, #7989 ) ;
#1314=SHAPE_REPRESENTATION ( 'hex thin nut chamfered gradeab_iso_ISO - 4035 - M5 - N', ( #1587 ), #2305 ) ;
#1328=PRODUCT_DEFINITION ( 'UNKNOWN', '', #2448, #227 ) ;
#1338=CARTESIAN_POINT ( 'NONE',  ( -1.321505333908963742, 3.855830693249141738, -2.665789719053469398 ) ) ;
#1341=ORIENTED_EDGE ( 'NONE', *, *, #6915, .T. ) ;
#1344=ORIENTED_EDGE ( 'NONE', *, *, #4461, .T. ) ;
#1348=CARTESIAN_POINT ( 'NONE',  ( 0.000000000000000000, 0.000000000000000000, -25.03750572909317285 ) ) ;
#1351=CARTESIAN_POINT ( 'NONE',  ( 1.257674520083185143E-14, 4.618802153517020948, -0.3572655899081733644 ) ) ;
#1379=SURFACE_SIDE_STYLE ('',( #7058 ) ) ;
#1380=EDGE_LOOP ( 'NONE', ( #4374, #4573, #4787 ) ) ;
#1386=ADVANCED_FACE ( 'NONE', ( #1273 ), #6107, .T. ) ;
#1392=VERTEX_POINT ( 'NONE', #4706 ) ;
#1409=CARTESIAN_POINT ( 'NONE',  ( 2.000000000000027089, 3.464101615137739731, -2.700000000000001066 ) ) ;
#1417=ORIENTED_EDGE ( 'NONE', *, *, #63, .F. ) ;
#1418=ORIENTED_EDGE ( 'NONE', *, *, #2801, .F. ) ;
#1424=CARTESIAN_POINT ( 'NONE',  ( 4.000000000000003553, 2.309401076758480720, -2.700000000000000178 ) ) ;
#1442=ADVANCED_FACE ( 'NONE', ( #2094 ), #6321, .F. ) ;
#1451=CARTESIAN_POINT ( 'NONE',  ( -4.000000000000000000, -2.309401076758531346, -0.3572655899081733644 ) ) ;
#1454=CARTESIAN_POINT ( 'NONE',  ( 1.257674520083185143E-14, 4.618802153517020948, -0.3572655899081733644 ) ) ;
#1456=CARTESIAN_POINT ( 'NONE',  ( 3.344563996438206122, 2.687817229851463097, -0.1586754815284832643 ) ) ;
#1458=CARTESIAN_POINT ( 'NONE',  ( -4.000000000000000000, -2.309401076758531346, -2.342734410091827701 ) ) ;
#1468=ADVANCED_FACE ( 'NONE', ( #3420 ), #251, .T. ) ;
#1473=ORIENTED_EDGE ( 'NONE', *, *, #2612, .F. ) ;
#1479=CARTESIAN_POINT ( 'NONE',  ( 0.000000000000000000, 0.000000000000000000, -2.674599999999998978 ) ) ;
#1480=CARTESIAN_POINT ( 'NONE',  ( 0.000000000000000000, 0.000000000000000000, -2.700000000000001066 ) ) ;
#1490=DIRECTION ( 'NONE',  ( 0.000000000000000000, 0.000000000000000000, -1.000000000000000000 ) ) ;
#1491=FILL_AREA_STYLE ('',( #774 ) ) ;
#1500=EDGE_CURVE ( 'NONE', #8121, #6469, #2961, .T. ) ;
#1521=EDGE_CURVE ( 'NONE', #6523, #2846, #8020, .T. ) ;
#1522=CARTESIAN_POINT ( 'NONE',  ( 0.000000000000000000, 0.000000000000000000, -0.2800830152838832965 ) ) ;
#1526=CARTESIAN_POINT ( 'NONE',  ( 2.000000000000027089, 3.464101615137739731, 0.000000000000000000 ) ) ;
#1535=CARTESIAN_POINT ( 'NONE',  ( 4.000000000000004441, -1.549102112939113152, -2.542104661404056554 ) ) ;
#1543=ORIENTED_EDGE ( 'NONE', *, *, #5800, .F. ) ;
#1556=EDGE_CURVE ( 'NONE', #2129, #2623, #1668, .T. ) ;
#1564=CARTESIAN_POINT ( 'NONE',  ( -2.000000000000022649, -3.464101615137742396, 0.000000000000000000 ) ) ;
#1587=AXIS2_PLACEMENT_3D ( 'NONE', #3942, #5152, #6454 ) ;
#1591=ORIENTED_EDGE ( 'NONE', *, *, #1184, .F. ) ;
#1592=ADVANCED_FACE ( 'NONE', ( #5591 ), #1820, .T. ) ;
#1593=CIRCLE ( 'NONE', #6223, 4.000000000000000000 ) ;
#1602=DIRECTION ( 'NONE',  ( -0.000000000000000000, -0.000000000000000000, 1.000000000000000000 ) ) ;
#1603=DIRECTION ( 'NONE',  ( 0.000000000000000000, -0.000000000000000000, 1.000000000000000000 ) ) ;
#1608=ORIENTED_EDGE ( 'NONE', *, *, #4702, .F. ) ;
#1619=EDGE_LOOP ( 'NONE', ( #7400, #7255, #2248, #689, #7018, #5429 ) ) ;
#1629=ORIENTED_EDGE ( 'NONE', *, *, #1128, .T. ) ;
#1652=CARTESIAN_POINT ( 'NONE',  ( -2.339468227445728576, -3.268109542640674547, -1.759456838036632033E-14 ) ) ;
#1656=LINE ( 'NONE', #348, #6654 ) ;
#1667=EDGE_CURVE ( 'NONE', #3249, #6523, #5197, .T. ) ;
#1668=B_SPLINE_CURVE_WITH_KNOTS ( 'NONE', 3,
 ( #7322, #1810, #4835, #4294, #1047, #4875 ),
 .UNSPECIFIED., .F., .F.,
 ( 4, 2, 4 ),
 ( 0.006456566858647417445, 0.007625406818786684658, 0.008794246778925951871 ),
 .UNSPECIFIED. ) ;
#1686=ORIENTED_EDGE ( 'NONE', *, *, #309, .T. ) ;
#1689=CARTESIAN_POINT ( 'NONE',  ( 3.344563996438205677, 2.687817229851463097, -2.541324518471518079 ) ) ;
#1691=DIRECTION ( 'NONE',  ( -0.000000000000000000, -0.000000000000000000, 1.000000000000000000 ) ) ;
#1701=CARTESIAN_POINT ( 'NONE',  ( 1.321505333908969293, -3.855830693249185703, -0.03421028094655650942 ) ) ;
#1720=PRESENTATION_STYLE_ASSIGNMENT (( #4203 ) ) ;
#1741=CARTESIAN_POINT ( 'NONE',  ( 3.999999999999989786, -2.309401076758547777, -0.3572655899081733644 ) ) ;
#1752=CARTESIAN_POINT ( 'NONE',  ( 4.000000000000003553, 2.309401076758524685, -2.342734410091827701 ) ) ;
#1754=CARTESIAN_POINT ( 'NONE',  ( -4.000000000000000000, -0.7779732554280791579, -0.03354435108167821283 ) ) ;
#1775=ORIENTED_EDGE ( 'NONE', *, *, #2547, .F. ) ;
#1781=CARTESIAN_POINT ( 'NONE',  ( 0.000000000000000000, 0.000000000000000000, -0.3080913168122707546 ) ) ;
#1788=COLOUR_RGB ( '', 0.08235294, 0.09019608, 0.10196078) ;
#1802=PRODUCT_DEFINITION_SHAPE ( 'NONE', 'NONE',  #1328 ) ;
#1807=SHAPE_REPRESENTATION_RELATIONSHIP ( 'NONE' , 'NONE' ,  #1314, #7232 ) ;
#1810=CARTESIAN_POINT ( 'NONE',  ( 4.000000000000003553, 0.3904826640788058301, -2.020173579201506309E-15 ) ) ;
#1820=CONICAL_SURFACE ( 'NONE', #3276, 4.000000000000000000, 1.047197551196595855 ) ;
#1823=ADVANCED_FACE ( 'NONE', ( #6716 ), #226, .T. ) ;
#1825=FACE_OUTER_BOUND ( 'NONE', #4648, .T. ) ;
#1851=ORIENTED_EDGE ( 'NONE', *, *, #6508, .F. ) ;
#1860=CIRCLE ( 'NONE', #907, 4.000000000000000000 ) ;
#1871=CARTESIAN_POINT ( 'NONE',  ( 0.000000000000000000, 0.000000000000000000, -2.700000000000001066 ) ) ;
#1879=ORIENTED_EDGE ( 'NONE', *, *, #7922, .T. ) ;
#1881=CARTESIAN_POINT ( 'NONE',  ( -4.000000000000000000, -2.309401076758531346, -2.342734410091827701 ) ) ;
#1887=EDGE_LOOP ( 'NONE', ( #7113, #3158, #1286, #7615 ) ) ;
#1894=DIRECTION ( 'NONE',  ( -1.000000000000000000, 0.000000000000000000, 0.000000000000000000 ) ) ;
#1898=EDGE_CURVE ( 'NONE', #3553, #3165, #6330, .T. ) ;
#1920=CARTESIAN_POINT ( 'NONE',  ( -4.000000000000000000, 2.309401076758496263, -0.3572655899081631503 ) ) ;
#1948=ADVANCED_FACE ( 'NONE', ( #4312, #6308 ), #7555, .F. ) ;
#1962=CARTESIAN_POINT ( 'NONE',  ( -4.000000000000000000, 1.935983797701054998, -0.2494693066162268769 ) ) ;
#2012=CARTESIAN_POINT ( 'NONE',  ( -4.000000000000000000, -0.7779732554280796020, -2.666455648918322208 ) ) ;
#2022=ORIENTED_EDGE ( 'NONE', *, *, #3930, .F. ) ;
#2075=EDGE_CURVE ( 'NONE', #855, #1392, #8118, .T. ) ;
#2077=EDGE_LOOP ( 'NONE', ( #2293, #8146, #5181, #7575 ) ) ;
#2083=AXIS2_PLACEMENT_3D ( 'NONE', #7209, #4180, #7833 ) ;
#2084=AXIS2_PLACEMENT_3D ( 'NONE', #2485, #2977, #3743 ) ;
#2085=CARTESIAN_POINT ( 'NONE',  ( 2.099999999999999645, 0.000000000000000000, -0.2800830152838832965 ) ) ;
#2088=EDGE_LOOP ( 'NONE', ( #5858, #38, #365, #740, #1417, #6513 ) ) ;
#2094=FACE_OUTER_BOUND ( 'NONE', #6279, .T. ) ;
#2097=CIRCLE ( 'NONE', #6736, 3.999999999999999112 ) ;
#2105=ADVANCED_FACE ( 'NONE', ( #5384 ), #4132, .F. ) ;
#2129=VERTEX_POINT ( 'NONE', #6619 ) ;
#2138=CARTESIAN_POINT ( 'NONE',  ( 2.000000000000027089, 3.464101615137739731, -2.700000000000001066 ) ) ;
#2166=DIRECTION ( 'NONE',  ( -0.000000000000000000, -0.000000000000000000, 1.000000000000000000 ) ) ;
#2167=EDGE_CURVE ( 'NONE', #6726, #4663, #5600, .T. ) ;
#2169=CARTESIAN_POINT ( 'NONE',  ( 3.999999999999989786, -2.309401076758547777, -0.3572655899081733644 ) ) ;
#2176=CARTESIAN_POINT ( 'NONE',  ( 0.6543461111163455524, 4.241015250120812929, -2.560849780464856895 ) ) ;
#2177=B_SPLINE_CURVE_WITH_KNOTS ( 'NONE', 3,
 ( #7383, #5525, #1701, #4234, #3655, #444 ),
 .UNSPECIFIED., .F., .F.,
 ( 4, 2, 4 ),
 ( 0.002336974151641521731, 0.003500975885716454527, 0.004664977619791387323 ),
 .UNSPECIFIED. ) ;
#2183=CARTESIAN_POINT ( 'NONE',  ( 3.673643420401898840, 2.497823135841254150, -2.451519936625006668 ) ) ;
#2194=ORIENTED_EDGE ( 'NONE', *, *, #3750, .F. ) ;
#2214=CARTESIAN_POINT ( 'NONE',  ( -1.318516776095820964, -3.857556137907092175, -1.717345860808523723E-14 ) ) ;
#2227=AXIS2_PLACEMENT_3D ( 'NONE', #2771, #1490, #7834 ) ;
#2233=DIRECTION ( 'NONE',  ( -0.5000000000000024425, 0.8660254037844373753, 0.000000000000000000 ) ) ;
#2248=ORIENTED_EDGE ( 'NONE', *, *, #5800, .T. ) ;
#2268=ORIENTED_EDGE ( 'NONE', *, *, #4064, .T. ) ;
#2270=CARTESIAN_POINT ( 'NONE',  ( 0.000000000000000000, 0.000000000000000000, -2.700000000000001066 ) ) ;
#2280=ORIENTED_EDGE ( 'NONE', *, *, #5761, .T. ) ;
#2286=CIRCLE ( 'NONE', #3619, 3.999999999999999112 ) ;
#2288=DIRECTION ( 'NONE',  ( 0.000000000000000000, 0.000000000000000000, -1.000000000000000000 ) ) ;
#2293=ORIENTED_EDGE ( 'NONE', *, *, #3907, .F. ) ;
#2294=B_SPLINE_CURVE_WITH_KNOTS ( 'NONE', 3,
 ( #1741, #3681, #4399, #5684, #8201, #2528 ),
 .UNSPECIFIED., .F., .F.,
 ( 4, 2, 4 ),
 ( 0.004120275011746849653, 0.005288420935197133549, 0.006456566858647417445 ),
 .UNSPECIFIED. ) ;
#2305=( GEOMETRIC_REPRESENTATION_CONTEXT ( 3 ) GLOBAL_UNCERTAINTY_ASSIGNED_CONTEXT ( ( #6548 ) ) GLOBAL_UNIT_ASSIGNED_CONTEXT ( ( #2424, #4965, #3133 ) ) REPRESENTATION_CONTEXT ( 'NONE', 'WORKASPACE' ) );
#2332=DIRECTION ( 'NONE',  ( -0.000000000000000000, -0.000000000000000000, 1.000000000000000000 ) ) ;
#2333=ORIENTED_EDGE ( 'NONE', *, *, #3443, .T. ) ;
#2401=DIRECTION ( 'NONE',  ( 0.000000000000000000, 0.000000000000000000, 1.000000000000000000 ) ) ;
#2411=CARTESIAN_POINT ( 'NONE',  ( 4.000000000000003553, 2.309401076758524685, -0.3572655899081733644 ) ) ;
#2416=ORIENTED_EDGE ( 'NONE', *, *, #6836, .T. ) ;
#2424=( LENGTH_UNIT ( ) NAMED_UNIT ( * ) SI_UNIT ( .MILLI., .METRE. ) );
#2427=DIRECTION ( 'NONE',  ( 0.000000000000000000, 0.000000000000000000, -1.000000000000000000 ) ) ;
#2430=EDGE_CURVE ( 'NONE', #6596, #4714, #6930, .T. ) ;
#2432=EDGE_CURVE ( 'NONE', #4613, #5533, #1656, .T. ) ;
#2442=DIRECTION ( 'NONE',  ( 1.000000000000000000, 0.000000000000000000, 0.000000000000000000 ) ) ;
#2448=PRODUCT_DEFINITION_FORMATION_WITH_SPECIFIED_SOURCE ( 'ANY', '', #5512, .NOT_KNOWN. ) ;
#2471=CARTESIAN_POINT ( 'NONE',  ( -2.000000000000009770, 3.464101615137749057, -2.700000000000001066 ) ) ;
#2480=CARTESIAN_POINT ( 'NONE',  ( -2.500000000000002220, 3.061616997868386099E-16, -25.03750572909317285 ) ) ;
#2485=CARTESIAN_POINT ( 'NONE',  ( 0.000000000000000000, 0.000000000000000000, 0.000000000000000000 ) ) ;
#2490=CARTESIAN_POINT ( 'NONE',  ( -3.345653888883663551, 2.687187980154699840, -2.560849780464863557 ) ) ;
#2491=CARTESIAN_POINT ( 'NONE',  ( -4.000000000000000000, 0.7862748000878055921, -0.03447227762756575886 ) ) ;
#2501=EDGE_LOOP ( 'NONE', ( #5348, #4507, #3919, #4076 ) ) ;
#2504=AXIS2_PLACEMENT_3D ( 'NONE', #2864, #2288, #2950 ) ;
#2507=B_SPLINE_CURVE_WITH_KNOTS ( 'NONE', 3,
 ( #1409, #5314, #5922, #1689, #2183, #3516 ),
 .UNSPECIFIED., .F., .F.,
 ( 4, 2, 4 ),
 ( 0.002336974151641575941, 0.003500975885716452358, 0.004664977619791328342 ),
 .UNSPECIFIED. ) ;
#2528=CARTESIAN_POINT ( 'NONE',  ( 4.000000000000000000, 0.000000000000000000, 0.000000000000000000 ) ) ;
#2533=VECTOR ( 'NONE', #1281, 1000.000000000000000 ) ;
#2540=CARTESIAN_POINT ( 'NONE',  ( -2.000000000000009770, 3.464101615137749057, 0.000000000000000000 ) ) ;
#2543=CARTESIAN_POINT ( 'NONE',  ( 0.000000000000000000, 0.000000000000000000, -2.700000000000000178 ) ) ;
#2547=EDGE_CURVE ( 'NONE', #1258, #6761, #5112, .T. ) ;
#2554=EDGE_LOOP ( 'NONE', ( #6971, #1629, #7451, #3710, #429, #1418 ) ) ;
#2559=CARTESIAN_POINT ( 'NONE',  ( -2.678494666091065124, -3.072372537026388351, -2.665789719053451634 ) ) ;
#2579=ORIENTED_EDGE ( 'NONE', *, *, #5761, .F. ) ;
#2586=ORIENTED_EDGE ( 'NONE', *, *, #4702, .T. ) ;
#2599=B_SPLINE_CURVE_WITH_KNOTS ( 'NONE', 3,
 ( #1920, #7054, #5653, #2540 ),
 .UNSPECIFIED., .F., .F.,
 ( 4, 4 ),
 ( 2.380737581620913884E-07, 0.002336974151641539512 ),
 .UNSPECIFIED. ) ;
#2604=CARTESIAN_POINT ( 'NONE',  ( 2.500000000000002220, 3.061616997868386099E-16, -2.674599999999998978 ) ) ;
#2612=EDGE_CURVE ( 'NONE', #3286, #6468, #2286, .T. ) ;
#2620=DIRECTION ( 'NONE',  ( 0.000000000000000000, 0.000000000000000000, 1.000000000000000000 ) ) ;
#2623=VERTEX_POINT ( 'NONE', #2411 ) ;
#2630=DIRECTION ( 'NONE',  ( -1.000000000000000000, -3.552713678800500929E-15, 0.000000000000000000 ) ) ;
#2658=AXIS2_PLACEMENT_3D ( 'NONE', #7823, #1603, #7938 ) ;
#2672=CARTESIAN_POINT ( 'NONE',  ( 0.000000000000000000, 0.000000000000000000, -2.700000000000000178 ) ) ;
#2690=AXIS2_PLACEMENT_3D ( 'NONE', #3430, #970, #4800 ) ;
#2694=DIRECTION ( 'NONE',  ( 0.000000000000000000, 0.000000000000000000, -1.000000000000000000 ) ) ;
#2706=EDGE_CURVE ( 'NONE', #4613, #7226, #3226, .T. ) ;
#2719=CARTESIAN_POINT ( 'NONE',  ( 2.099999999999999645, 0.000000000000000000, -2.700000000000000178 ) ) ;
#2720=DIRECTION ( 'NONE',  ( 1.000000000000000000, 0.000000000000000000, 0.000000000000000000 ) ) ;
#2726=CYLINDRICAL_SURFACE ( 'NONE', #5844, 2.099999999999999645 ) ;
#2727=EDGE_CURVE ( 'NONE', #2846, #3286, #4335, .T. ) ;
#2742=DIRECTION ( 'NONE',  ( -1.000000000000000000, 0.000000000000000000, 0.000000000000000000 ) ) ;
#2770=CIRCLE ( 'NONE', #4368, 2.099999999999999645 ) ;
#2771=CARTESIAN_POINT ( 'NONE',  ( 0.000000000000000000, 0.000000000000000000, 0.000000000000000000 ) ) ;
#2776=CIRCLE ( 'NONE', #7418, 2.500000000000000444 ) ;
#2801=EDGE_CURVE ( 'NONE', #8121, #3249, #5040, .T. ) ;
#2806=LINE ( 'NONE', #2719, #5730 ) ;
#2817=CARTESIAN_POINT ( 'NONE',  ( 0.000000000000000000, 0.000000000000000000, -2.394516984716111185 ) ) ;
#2829=ADVANCED_FACE ( 'NONE', ( #110, #3328 ), #6355, .T. ) ;
#2845=CARTESIAN_POINT ( 'NONE',  ( 1.084202172485504434E-14, 4.618802153517020948, -2.342734410091827701 ) ) ;
#2846=VERTEX_POINT ( 'NONE', #1451 ) ;
#2864=CARTESIAN_POINT ( 'NONE',  ( 0.000000000000000000, 0.000000000000000000, -0.2800830152838832965 ) ) ;
#2882=CARTESIAN_POINT ( 'NONE',  ( 1.318516776095787879, 3.857556137907072635, -2.700000000000003730 ) ) ;
#2890=DIRECTION ( 'NONE',  ( 0.000000000000000000, -0.000000000000000000, 1.000000000000000000 ) ) ;
#2907=CARTESIAN_POINT ( 'NONE',  ( 4.000000000000000000, 0.000000000000000000, -2.700000000000001066 ) ) ;
#2921=DIRECTION ( 'NONE',  ( 0.000000000000000000, 0.000000000000000000, 1.000000000000000000 ) ) ;
#2945=CARTESIAN_POINT ( 'NONE',  ( -3.999999999999999112, 1.557668341133520373, -2.540303434304243879 ) ) ;
#2950=DIRECTION ( 'NONE',  ( 1.000000000000000000, 0.000000000000000000, 0.000000000000000000 ) ) ;
#2961=LINE ( 'NONE', #4206, #5001 ) ;
#2977=DIRECTION ( 'NONE',  ( -0.000000000000000000, 0.000000000000000000, -1.000000000000000000 ) ) ;
#3013=CARTESIAN_POINT ( 'NONE',  ( -4.000000000000000000, 0.000000000000000000, -2.700000000000000178 ) ) ;
#3023=LINE ( 'NONE', #6227, #3976 ) ;
#3034=ADVANCED_FACE ( 'NONE', ( #5923 ), #4600, .T. ) ;
#3045=CONICAL_SURFACE ( 'NONE', #6494, 2.060000000000000941, 0.9599310885968777018 ) ;
#3046=ORIENTED_EDGE ( 'NONE', *, *, #505, .T. ) ;
#3053=EDGE_CURVE ( 'NONE', #7269, #4852, #8173, .T. ) ;
#3069=AXIS2_PLACEMENT_3D ( 'NONE', #7088, #5081, #61 ) ;
#3074=CARTESIAN_POINT ( 'NONE',  ( -3.999999999999999112, 1.935983797701082976, -2.450530693383766501 ) ) ;
#3117=CARTESIAN_POINT ( 'NONE',  ( 2.000000000000010658, -3.464101615137748169, -2.700000000000001066 ) ) ;
#3118=DIRECTION ( 'NONE',  ( 0.000000000000000000, 0.000000000000000000, 1.000000000000000000 ) ) ;
#3119=CARTESIAN_POINT ( 'NONE',  ( -4.000000000000000000, -2.309401076758531346, -0.3572655899081733644 ) ) ;
#3122=AXIS2_PLACEMENT_3D ( 'NONE', #1522, #7752, #5388 ) ;
#3130=FACE_OUTER_BOUND ( 'NONE', #1887, .T. ) ;
#3131=FACE_OUTER_BOUND ( 'NONE', #1619, .T. ) ;
#3133=( NAMED_UNIT ( * ) SI_UNIT ( $, .STERADIAN. ) SOLID_ANGLE_UNIT ( ) );
#3158=ORIENTED_EDGE ( 'NONE', *, *, #6836, .F. ) ;
#3159=CARTESIAN_POINT ( 'NONE',  ( 2.000000000000010658, -3.464101615137748169, -2.700000000000001066 ) ) ;
#3161=CARTESIAN_POINT ( 'NONE',  ( -2.681483223904233881, 3.070647092368429032, -2.700000000000003730 ) ) ;
#3165=VERTEX_POINT ( 'NONE', #3232 ) ;
#3175=VECTOR ( 'NONE', #3493, 1000.000000000000000 ) ;
#3212=CARTESIAN_POINT ( 'NONE',  ( -4.000000000000000000, 0.000000000000000000, 0.000000000000000000 ) ) ;
#3219=EDGE_CURVE ( 'NONE', #4714, #4852, #5679, .T. ) ;
#3224=B_SPLINE_CURVE_WITH_KNOTS ( 'NONE', 3,
 ( #3574, #3454, #6014, #5365, #275, #1752 ),
 .UNSPECIFIED., .F., .F.,
 ( 4, 2, 4 ),
 ( 0.006456566858647416578, 0.007625406818786683791, 0.008794246778925951871 ),
 .UNSPECIFIED. ) ;
#3226=B_SPLINE_CURVE_WITH_KNOTS ( 'NONE', 3,
 ( #8096, #2490, #3161, #4319 ),
 .UNSPECIFIED., .F., .F.,
 ( 4, 4 ),
 ( 2.380737581781596034E-07, 0.002336974151641540379 ),
 .UNSPECIFIED. ) ;
#3232=CARTESIAN_POINT ( 'NONE',  ( -2.000000000000022649, -3.464101615137742396, 0.000000000000000000 ) ) ;
#3241=ORIENTED_EDGE ( 'NONE', *, *, #3907, .T. ) ;
#3246=B_SPLINE_CURVE_WITH_KNOTS ( 'NONE', 3,
 ( #3752, #488, #4410, #7517 ),
 .UNSPECIFIED., .F., .F.,
 ( 4, 4 ),
 ( 2.380737581781827115E-07, 0.002336974151641521731 ),
 .UNSPECIFIED. ) ;
#3247=CARTESIAN_POINT ( 'NONE',  ( -0.3263565795980845063, 4.430380094434251070, -2.451519936624993345 ) ) ;
#3249=VERTEX_POINT ( 'NONE', #7371 ) ;
#3268=CARTESIAN_POINT ( 'NONE',  ( 2.500000000000002220, 3.061616997868386099E-16, -2.674599999999998978 ) ) ;
#3272=ADVANCED_FACE ( 'NONE', ( #5946 ), #4878, .T. ) ;
#3276=AXIS2_PLACEMENT_3D ( 'NONE', #8110, #2427, #6952 ) ;
#3286=VERTEX_POINT ( 'NONE', #4667 ) ;
#3314=DIRECTION ( 'NONE',  ( -1.000000000000000000, 0.000000000000000000, 0.000000000000000000 ) ) ;
#3328=FACE_OUTER_BOUND ( 'NONE', #4863, .T. ) ;
#3335=ORIENTED_EDGE ( 'NONE', *, *, #1556, .T. ) ;
#3337=VERTEX_POINT ( 'NONE', #4015 ) ;
#3364=VERTEX_POINT ( 'NONE', #2169 ) ;
#3381=FACE_OUTER_BOUND ( 'NONE', #5683, .T. ) ;
#3387=ADVANCED_FACE ( 'NONE', ( #5414 ), #4740, .T. ) ;
#3389=DIRECTION ( 'NONE',  ( 0.5000000000000026645, -0.8660254037844372643, 0.000000000000000000 ) ) ;
#3407=FACE_OUTER_BOUND ( 'NONE', #4700, .T. ) ;
#3419=CIRCLE ( 'NONE', #1160, 2.500000000000002220 ) ;
#3420=FACE_OUTER_BOUND ( 'NONE', #2554, .T. ) ;
#3426=AXIS2_PLACEMENT_3D ( 'NONE', #6193, #4291, #5539 ) ;
#3427=CARTESIAN_POINT ( 'NONE',  ( -0.6543461111163948463, -4.241015250120822699, -0.1391502195351549120 ) ) ;
#3430=CARTESIAN_POINT ( 'NONE',  ( 0.000000000000000000, 0.000000000000000000, 3.469446951953614189E-15 ) ) ;
#3434=PLANE ( 'NONE',  #4351 ) ;
#3443=EDGE_CURVE ( 'NONE', #7226, #4246, #3732, .T. ) ;
#3450=AXIS2_PLACEMENT_3D ( 'NONE', #4170, #7326, #210 ) ;
#3452=( GEOMETRIC_REPRESENTATION_CONTEXT ( 3 ) GLOBAL_UNCERTAINTY_ASSIGNED_CONTEXT ( ( #7365 ) ) GLOBAL_UNIT_ASSIGNED_CONTEXT ( ( #5891, #7683, #70 ) ) REPRESENTATION_CONTEXT ( 'NONE', 'WORKASPACE' ) );
#3454=CARTESIAN_POINT ( 'NONE',  ( 4.000000000000003553, 0.3904826640788058856, -2.699999999999998401 ) ) ;
#3483=DIRECTION ( 'NONE',  ( -1.000000000000000000, 0.000000000000000000, 0.000000000000000000 ) ) ;
#3491=CARTESIAN_POINT ( 'NONE',  ( 4.000000000000003553, -0.3902508023145564442, -2.699999999999998845 ) ) ;
#3493=DIRECTION ( 'NONE',  ( 0.000000000000000000, 0.000000000000000000, 1.000000000000000000 ) ) ;
#3497=ORIENTED_EDGE ( 'NONE', *, *, #6688, .T. ) ;
#3516=CARTESIAN_POINT ( 'NONE',  ( 4.000000000000003553, 2.309401076758524685, -2.342734410091827701 ) ) ;
#3528=CARTESIAN_POINT ( 'NONE',  ( 4.000000000000003553, -1.933795701539621437, -2.451162342337698252 ) ) ;
#3536=ORIENTED_EDGE ( 'NONE', *, *, #3809, .T. ) ;
#3553=VERTEX_POINT ( 'NONE', #3884 ) ;
#3558=CARTESIAN_POINT ( 'NONE',  ( -4.000000000000000000, -2.309401076758531346, -0.3572655899081733644 ) ) ;
#3562=LINE ( 'NONE', #6094, #7027 ) ;
#3567=VECTOR ( 'NONE', #6475, 1000.000000000000114 ) ;
#3574=CARTESIAN_POINT ( 'NONE',  ( 4.000000000000000000, 0.000000000000000000, -2.700000000000001066 ) ) ;
#3580=CIRCLE ( 'NONE', #2658, 4.000000000000000888 ) ;
#3592=CARTESIAN_POINT ( 'NONE',  ( -4.000000000000000000, -2.309401076758525573, -2.700000000000000178 ) ) ;
#3614=VERTEX_POINT ( 'NONE', #1351 ) ;
#3619=AXIS2_PLACEMENT_3D ( 'NONE', #5366, #4237, #902 ) ;
#3620=DIRECTION ( 'NONE',  ( -0.000000000000000000, -0.000000000000000000, 1.000000000000000000 ) ) ;
#3645=DIRECTION ( 'NONE',  ( -1.000000000000000000, 0.000000000000000000, 0.000000000000000000 ) ) ;
#3647=EDGE_CURVE ( 'NONE', #4246, #3249, #6241, .T. ) ;
#3655=CARTESIAN_POINT ( 'NONE',  ( 0.3263565795980692408, -4.430380094434308802, -0.2484800633750388066 ) ) ;
#3670=CARTESIAN_POINT ( 'NONE',  ( 0.000000000000000000, 0.000000000000000000, -2.700000000000001066 ) ) ;
#3681=CARTESIAN_POINT ( 'NONE',  ( 4.000000000000003553, -1.933795701539621659, -0.2488376576623028413 ) ) ;
#3684=DIRECTION ( 'NONE',  ( 1.000000000000000000, 0.000000000000000000, 0.000000000000000000 ) ) ;
#3708=B_SPLINE_CURVE_WITH_KNOTS ( 'NONE', 3,
 ( #175, #5381, #7893, #6659, #7937, #4672 ),
 .UNSPECIFIED., .F., .F.,
 ( 4, 2, 4 ),
 ( 0.002336974151641539512, 0.003500975885716449323, 0.004664977619791359567 ),
 .UNSPECIFIED. ) ;
#3710=ORIENTED_EDGE ( 'NONE', *, *, #1521, .F. ) ;
#3712=DIRECTION ( 'NONE',  ( -1.000000000000000000, 0.000000000000000000, 0.000000000000000000 ) ) ;
#3727=AXIS2_PLACEMENT_3D ( 'NONE', #1871, #8084, #3684 ) ;
#3732=CIRCLE ( 'NONE', #3426, 4.000000000000000888 ) ;
#3734=CIRCLE ( 'NONE', #6243, 3.999999999999999112 ) ;
#3743=DIRECTION ( 'NONE',  ( -1.000000000000000000, 0.000000000000000000, 0.000000000000000000 ) ) ;
#3748=CYLINDRICAL_SURFACE ( 'NONE', #4895, 2.099999999999999645 ) ;
#3750=EDGE_CURVE ( 'NONE', #4602, #1392, #825, .T. ) ;
#3752=CARTESIAN_POINT ( 'NONE',  ( 3.999999999999989786, -2.309401076758547777, -0.3572655899081733644 ) ) ;
#3766=ADVANCED_FACE ( 'NONE', ( #3407 ), #164, .F. ) ;
#3771=EDGE_CURVE ( 'NONE', #5524, #855, #4007, .T. ) ;
#3795=ORIENTED_EDGE ( 'NONE', *, *, #2706, .T. ) ;
#3798=EDGE_LOOP ( 'NONE', ( #1344, #564, #1775 ) ) ;
#3800=CYLINDRICAL_SURFACE ( 'NONE', #6357, 2.500000000000002220 ) ;
#3809=EDGE_CURVE ( 'NONE', #4663, #7226, #362, .T. ) ;
#3810=B_SPLINE_CURVE_WITH_KNOTS ( 'NONE', 3,
 ( #701, #7608, #1338, #4994, #3247, #7514 ),
 .UNSPECIFIED., .F., .F.,
 ( 4, 2, 4 ),
 ( 0.002336974151641540379, 0.003500975885716449323, 0.004664977619791357832 ),
 .UNSPECIFIED. ) ;
#3817=CARTESIAN_POINT ( 'NONE',  ( 0.000000000000000000, 0.000000000000000000, -2.700000000000001066 ) ) ;
#3819=ORIENTED_EDGE ( 'NONE', *, *, #2167, .F. ) ;
#3824=FACE_OUTER_BOUND ( 'NONE', #7646, .T. ) ;
#3846=CLOSED_SHELL ( 'NONE', ( #2105, #1442, #6536, #6569, #4049, #1823, #6764, #3766, #464, #1468, #7636, #1948, #2829, #4673, #3272, #1386, #3034, #3387, #4265, #7160, #7121, #5937, #810, #8071, #1592, #922, #964, #5339 ) ) ;
#3849=EDGE_LOOP ( 'NONE', ( #2194, #3046, #7524, #6022 ) ) ;
#3863=EDGE_LOOP ( 'NONE', ( #6824, #1341, #5143, #7767 ) ) ;
#3866=DIRECTION ( 'NONE',  ( -1.000000000000000000, 0.000000000000000000, 0.000000000000000000 ) ) ;
#3873=DIRECTION ( 'NONE',  ( -1.000000000000000000, 0.000000000000000000, 0.000000000000000000 ) ) ;
#3878=ORIENTED_EDGE ( 'NONE', *, *, #6916, .F. ) ;
#3882=DIRECTION ( 'NONE',  ( -0.000000000000000000, -0.000000000000000000, 1.000000000000000000 ) ) ;
#3884=CARTESIAN_POINT ( 'NONE',  ( 2.000000000000010658, -3.464101615137748169, 0.000000000000000000 ) ) ;
#3907=EDGE_CURVE ( 'NONE', #6596, #4602, #4732, .T. ) ;
#3917=CARTESIAN_POINT ( 'NONE',  ( -4.000000000000000000, 0.000000000000000000, -2.700000000000000178 ) ) ;
#3919=ORIENTED_EDGE ( 'NONE', *, *, #754, .T. ) ;
#3922=CARTESIAN_POINT ( 'NONE',  ( -4.000000000000000000, 2.309401076758496263, -2.700000000000000178 ) ) ;
#3930=EDGE_CURVE ( 'NONE', #5524, #4602, #5551, .T. ) ;
#3942=CARTESIAN_POINT ( 'NONE',  ( 0.000000000000000000, 0.000000000000000000, 0.000000000000000000 ) ) ;
#3945=VECTOR ( 'NONE', #1000, 1000.000000000000000 ) ;
#3955=ORIENTED_EDGE ( 'NONE', *, *, #3647, .T. ) ;
#3972=EDGE_CURVE ( 'NONE', #3364, #3553, #3246, .T. ) ;
#3976=VECTOR ( 'NONE', #8095, 1000.000000000000114 ) ;
#3985=AXIS2_PLACEMENT_3D ( 'NONE', #7983, #5913, #4674 ) ;
#3993=CARTESIAN_POINT ( 'NONE',  ( 0.6543461111163468846, 4.241015250120812929, -0.1391502195351439208 ) ) ;
#3997=AXIS2_PLACEMENT_3D ( 'NONE', #3817, #6336, #5380 ) ;
#4007=LINE ( 'NONE', #4546, #7264 ) ;
#4015=CARTESIAN_POINT ( 'NONE',  ( 2.000000000000027089, 3.464101615137739731, 0.000000000000000000 ) ) ;
#4017=DIRECTION ( 'NONE',  ( 0.000000000000000000, 0.000000000000000000, -1.000000000000000000 ) ) ;
#4023=CARTESIAN_POINT ( 'NONE',  ( 2.000000000000027089, 3.464101615137739731, -2.700000000000001066 ) ) ;
#4041=ORIENTED_EDGE ( 'NONE', *, *, #7515, .F. ) ;
#4044=CARTESIAN_POINT ( 'NONE',  ( 0.000000000000000000, 0.000000000000000000, -2.674599999999998978 ) ) ;
#4049=ADVANCED_FACE ( 'NONE', ( #5780 ), #2726, .F. ) ;
#4051=CARTESIAN_POINT ( 'NONE',  ( 2.099999999999999645, 0.000000000000000000, -2.394516984716111185 ) ) ;
#4055=EDGE_LOOP ( 'NONE', ( #6187, #3241, #2022, #1591 ) ) ;
#4064=EDGE_CURVE ( 'NONE', #3337, #2623, #443, .T. ) ;
#4069=MANIFOLD_SOLID_BREP ( 'EndChamfer', #3846 ) ;
#4074=SHAPE_DEFINITION_REPRESENTATION ( #1802, #1314 ) ;
#4076=ORIENTED_EDGE ( 'NONE', *, *, #3771, .F. ) ;
#4082=AXIS2_PLACEMENT_3D ( 'NONE', #7706, #7080, #287 ) ;
#4099=CARTESIAN_POINT ( 'NONE',  ( -2.271448787322325728E-15, -4.618802153517061804, -2.700000000000000178 ) ) ;
#4110=CONICAL_SURFACE ( 'NONE', #3985, 4.000000000000000000, 1.047197551196595855 ) ;
#4112=MECHANICAL_DESIGN_GEOMETRIC_PRESENTATION_REPRESENTATION('',(#7288),#3452);
#4132=CYLINDRICAL_SURFACE ( 'NONE', #5874, 2.500000000000002220 ) ;
#4145=CARTESIAN_POINT ( 'NONE',  ( 1.155036213957052500E-14, 4.618802153517020059, -2.700000000000000178 ) ) ;
#4165=DIRECTION ( 'NONE',  ( 1.000000000000000000, 0.000000000000000000, 0.000000000000000000 ) ) ;
#4170=CARTESIAN_POINT ( 'NONE',  ( 0.000000000000000000, 0.000000000000000000, 0.000000000000000000 ) ) ;
#4179=CARTESIAN_POINT ( 'NONE',  ( 4.000000000000003553, 2.309401076758480720, -2.700000000000000178 ) ) ;
#4180=DIRECTION ( 'NONE',  ( -0.000000000000000000, -0.000000000000000000, 1.000000000000000000 ) ) ;
#4203=SURFACE_STYLE_USAGE ( .BOTH. , #8056 ) ;
#4206=CARTESIAN_POINT ( 'NONE',  ( -2.271448787322325728E-15, -4.618802153517061804, -2.700000000000000178 ) ) ;
#4217=ORIENTED_EDGE ( 'NONE', *, *, #5227, .T. ) ;
#4230=ORIENTED_EDGE ( 'NONE', *, *, #6800, .T. ) ;
#4234=CARTESIAN_POINT ( 'NONE',  ( 0.6554360035617808888, -4.240386000424090973, -0.1586754815285200126 ) ) ;
#4237=DIRECTION ( 'NONE',  ( -0.000000000000000000, 0.000000000000000000, -1.000000000000000000 ) ) ;
#4243=AXIS2_PLACEMENT_3D ( 'NONE', #4044, #2166, #4703 ) ;
#4246=VERTEX_POINT ( 'NONE', #3013 ) ;
#4250=CARTESIAN_POINT ( 'NONE',  ( 0.000000000000000000, 0.000000000000000000, 0.000000000000000000 ) ) ;
#4261=EDGE_CURVE ( 'NONE', #1258, #3364, #4349, .T. ) ;
#4265=ADVANCED_FACE ( 'NONE', ( #6927 ), #5062, .T. ) ;
#4291=DIRECTION ( 'NONE',  ( 0.000000000000000000, -0.000000000000000000, 1.000000000000000000 ) ) ;
#4294=CARTESIAN_POINT ( 'NONE',  ( 4.000000000000002665, 1.557668341133515932, -0.1596965656957575197 ) ) ;
#4302=EDGE_CURVE ( 'NONE', #7783, #2623, #7422, .T. ) ;
#4307=LINE ( 'NONE', #2480, #6589 ) ;
#4312=FACE_BOUND ( 'NONE', #1122, .T. ) ;
#4314=EDGE_LOOP ( 'NONE', ( #5601, #4456, #6248 ) ) ;
#4319=CARTESIAN_POINT ( 'NONE',  ( -2.000000000000009770, 3.464101615137749057, -2.700000000000001066 ) ) ;
#4335=B_SPLINE_CURVE_WITH_KNOTS ( 'NONE', 3,
 ( #3119, #1115, #5656, #1754, #4408, #5035 ),
 .UNSPECIFIED., .F., .F.,
 ( 4, 2, 4 ),
 ( 0.004120275011746842714, 0.005288420935197119671, 0.006456566858647395761 ),
 .UNSPECIFIED. ) ;
#4349=LINE ( 'NONE', #5023, #5193 ) ;
#4350=DIRECTION ( 'NONE',  ( 1.000000000000000000, 0.000000000000000000, 0.000000000000000000 ) ) ;
#4351=AXIS2_PLACEMENT_3D ( 'NONE', #4179, #7208, #4761 ) ;
#4368=AXIS2_PLACEMENT_3D ( 'NONE', #6171, #476, #3866 ) ;
#4374=ORIENTED_EDGE ( 'NONE', *, *, #6916, .T. ) ;
#4385=ORIENTED_EDGE ( 'NONE', *, *, #3219, .F. ) ;
#4393=EDGE_CURVE ( 'NONE', #4714, #6596, #2770, .T. ) ;
#4398=ORIENTED_EDGE ( 'NONE', *, *, #1667, .T. ) ;
#4399=CARTESIAN_POINT ( 'NONE',  ( 4.000000000000004441, -1.549102112939112486, -0.1578953385959447620 ) ) ;
#4408=CARTESIAN_POINT ( 'NONE',  ( -4.000000000000000000, -0.3902508023145541127, 1.101142831430590133E-17 ) ) ;
#4410=CARTESIAN_POINT ( 'NONE',  ( 2.681483223904246316, -3.070647092368467668, -2.032850044890171669E-14 ) ) ;
#4456=ORIENTED_EDGE ( 'NONE', *, *, #1128, .F. ) ;
#4461=EDGE_CURVE ( 'NONE', #1258, #397, #6653, .T. ) ;
#4495=ORIENTED_EDGE ( 'NONE', *, *, #4302, .T. ) ;
#4502=AXIS2_PLACEMENT_3D ( 'NONE', #1424, #2742, #5938 ) ;
#4506=VECTOR ( 'NONE', #3620, 1000.000000000000000 ) ;
#4507=ORIENTED_EDGE ( 'NONE', *, *, #3750, .T. ) ;
#4540=CARTESIAN_POINT ( 'NONE',  ( -4.000000000000000000, -1.933795701539609668, -2.451162342337703137 ) ) ;
#4546=CARTESIAN_POINT ( 'NONE',  ( 2.060000000000000941, 0.000000000000000000, -0.3080913168122707546 ) ) ;
#4564=CARTESIAN_POINT ( 'NONE',  ( 2.500000000000002220, 0.000000000000000000, -2.700000000000001066 ) ) ;
#4569=CARTESIAN_POINT ( 'NONE',  ( 4.000000000000003553, 2.309401076758524685, -0.3572655899081733644 ) ) ;
#4573=ORIENTED_EDGE ( 'NONE', *, *, #7218, .T. ) ;
#4600=CONICAL_SURFACE ( 'NONE', #2083, 4.000000000000000000, 1.047197551196595855 ) ;
#4602=VERTEX_POINT ( 'NONE', #7235 ) ;
#4613=VERTEX_POINT ( 'NONE', #5421 ) ;
#4614=DIRECTION ( 'NONE',  ( -1.000000000000000000, 1.776356839400250465E-15, 0.000000000000000000 ) ) ;
#4644=CARTESIAN_POINT ( 'NONE',  ( -1.318516776095820964, -3.857556137907092175, -2.699999999999984190 ) ) ;
#4648=EDGE_LOOP ( 'NONE', ( #5486, #3335, #7759 ) ) ;
#4663=VERTEX_POINT ( 'NONE', #2138 ) ;
#4667=CARTESIAN_POINT ( 'NONE',  ( -4.000000000000000000, 0.000000000000000000, 0.000000000000000000 ) ) ;
#4672=CARTESIAN_POINT ( 'NONE',  ( 1.257674520083185143E-14, 4.618802153517020948, -0.3572655899081733644 ) ) ;
#4673=ADVANCED_FACE ( 'NONE', ( #3381 ), #771, .T. ) ;
#4674=DIRECTION ( 'NONE',  ( -1.000000000000000000, 0.000000000000000000, 0.000000000000000000 ) ) ;
#4700=EDGE_LOOP ( 'NONE', ( #3878, #6221, #1244, #782, #4495, #6047 ) ) ;
#4702=EDGE_CURVE ( 'NONE', #6468, #3614, #3708, .T. ) ;
#4703=DIRECTION ( 'NONE',  ( 1.000000000000000000, 0.000000000000000000, 0.000000000000000000 ) ) ;
#4706=CARTESIAN_POINT ( 'NONE',  ( -2.500000000000000444, 3.061616997868384127E-16, 3.469446951953614189E-15 ) ) ;
#4714=VERTEX_POINT ( 'NONE', #4051 ) ;
#4728=CARTESIAN_POINT ( 'NONE',  ( -7.502679033599690683E-14, -4.618802153517020059, -2.342734410091827701 ) ) ;
#4731=CARTESIAN_POINT ( 'NONE',  ( -4.000000000000000000, 2.309401076758496263, -0.3572655899081631503 ) ) ;
#4732=LINE ( 'NONE', #950, #3175 ) ;
#4740=CONICAL_SURFACE ( 'NONE', #5546, 4.000000000000000000, 1.047197551196595855 ) ;
#4758=EDGE_LOOP ( 'NONE', ( #1473, #4041, #7220, #7303, #1879, #7852 ) ) ;
#4761=DIRECTION ( 'NONE',  ( -0.8660254037844347108, 0.5000000000000066613, 0.000000000000000000 ) ) ;
#4770=DIRECTION ( 'NONE',  ( -0.8660254037844372643, -0.5000000000000023315, 0.000000000000000000 ) ) ;
#4787=ORIENTED_EDGE ( 'NONE', *, *, #3972, .F. ) ;
#4800=DIRECTION ( 'NONE',  ( 1.000000000000000000, 0.000000000000000000, 0.000000000000000000 ) ) ;
#4835=CARTESIAN_POINT ( 'NONE',  ( 4.000000000000004441, 0.7862748000878159171, -0.03447227762756881198 ) ) ;
#4852=VERTEX_POINT ( 'NONE', #2604 ) ;
#4863=EDGE_LOOP ( 'NONE', ( #83, #5905, #6021, #6396, #5933, #647 ) ) ;
#4867=AXIS2_PLACEMENT_3D ( 'NONE', #5690, #1069, #6840 ) ;
#4875=CARTESIAN_POINT ( 'NONE',  ( 4.000000000000003553, 2.309401076758524685, -0.3572655899081733644 ) ) ;
#4876=ORIENTED_EDGE ( 'NONE', *, *, #7515, .T. ) ;
#4878=CONICAL_SURFACE ( 'NONE', #4082, 4.000000000000000000, 1.047197551196595855 ) ;
#4895=AXIS2_PLACEMENT_3D ( 'NONE', #2543, #3118, #5086 ) ;
#4935=CARTESIAN_POINT ( 'NONE',  ( 3.999999999999989786, -2.309401076758547777, -2.342734410091827701 ) ) ;
#4965=( NAMED_UNIT ( * ) PLANE_ANGLE_UNIT ( ) SI_UNIT ( $, .RADIAN. ) );
#4968=DIRECTION ( 'NONE',  ( -0.5000000000000057732, -0.8660254037844353769, 0.000000000000000000 ) ) ;
#4994=CARTESIAN_POINT ( 'NONE',  ( -0.6554360035617892155, 4.240386000424039459, -2.541324518471509641 ) ) ;
#5001=VECTOR ( 'NONE', #2921, 1000.000000000000000 ) ;
#5023=CARTESIAN_POINT ( 'NONE',  ( 4.000000000000003553, -2.309401076758539784, -2.700000000000000178 ) ) ;
#5035=CARTESIAN_POINT ( 'NONE',  ( -4.000000000000000000, 0.000000000000000000, 0.000000000000000000 ) ) ;
#5037=CARTESIAN_POINT ( 'NONE',  ( -4.000000000000000000, 1.557668341133497059, -0.1596965656957516910 ) ) ;
#5040=B_SPLINE_CURVE_WITH_KNOTS ( 'NONE', 3,
 ( #7753, #153, #4644, #5159 ),
 .UNSPECIFIED., .F., .F.,
 ( 4, 4 ),
 ( 2.380737582494440699E-07, 0.002336974151641604564 ),
 .UNSPECIFIED. ) ;
#5057=CARTESIAN_POINT ( 'NONE',  ( -2.000000000000022649, -3.464101615137742396, -2.700000000000001066 ) ) ;
#5062=CONICAL_SURFACE ( 'NONE', #3727, 4.000000000000000000, 1.047197551196595855 ) ;
#5081=DIRECTION ( 'NONE',  ( 0.000000000000000000, 0.000000000000000000, -1.000000000000000000 ) ) ;
#5086=DIRECTION ( 'NONE',  ( 1.000000000000000000, 0.000000000000000000, 0.000000000000000000 ) ) ;
#5112=B_SPLINE_CURVE_WITH_KNOTS ( 'NONE', 3,
 ( #318, #3528, #1535, #7916, #3491, #2907 ),
 .UNSPECIFIED., .F., .F.,
 ( 4, 2, 4 ),
 ( 0.004120275011746849653, 0.005288420935197133549, 0.006456566858647416578 ),
 .UNSPECIFIED. ) ;
#5140=EDGE_LOOP ( 'NONE', ( #300, #7700, #6556 ) ) ;
#5143=ORIENTED_EDGE ( 'NONE', *, *, #3053, .T. ) ;
#5149=EDGE_CURVE ( 'NONE', #4852, #7269, #7812, .T. ) ;
#5152=DIRECTION ( 'NONE',  ( 0.000000000000000000, 0.000000000000000000, 1.000000000000000000 ) ) ;
#5159=CARTESIAN_POINT ( 'NONE',  ( -2.000000000000022649, -3.464101615137742396, -2.700000000000001066 ) ) ;
#5161=CARTESIAN_POINT ( 'NONE',  ( 1.318516776095788767, 3.857556137907071747, 2.429570457523002859E-15 ) ) ;
#5162=PRESENTATION_STYLE_ASSIGNMENT (( #5925 ) ) ;
#5165=AXIS2_PLACEMENT_3D ( 'NONE', #2672, #80, #2630 ) ;
#5167=CARTESIAN_POINT ( 'NONE',  ( -4.000000000000000000, -1.549102112939103826, -2.542104661404059662 ) ) ;
#5173=PLANE ( 'NONE',  #7428 ) ;
#5181=ORIENTED_EDGE ( 'NONE', *, *, #1184, .T. ) ;
#5193=VECTOR ( 'NONE', #2401, 1000.000000000000000 ) ;
#5197=B_SPLINE_CURVE_WITH_KNOTS ( 'NONE', 3,
 ( #5057, #7101, #2559, #5211, #7726, #1458 ),
 .UNSPECIFIED., .F., .F.,
 ( 4, 2, 4 ),
 ( 0.002336974151641604564, 0.003500975885716477512, 0.004664977619791350026 ),
 .UNSPECIFIED. ) ;
#5211=CARTESIAN_POINT ( 'NONE',  ( -3.344563996438218556, -2.687817229851498624, -2.541324518471498983 ) ) ;
#5214=ORIENTED_EDGE ( 'NONE', *, *, #5149, .F. ) ;
#5227=EDGE_CURVE ( 'NONE', #6761, #4663, #1593, .T. ) ;
#5246=ORIENTED_EDGE ( 'NONE', *, *, #309, .F. ) ;
#5250=DIRECTION ( 'NONE',  ( 0.8191520442889896891, 0.000000000000000000, 0.5735764363510490460 ) ) ;
#5268=EDGE_LOOP ( 'NONE', ( #4385, #7546, #6119, #5214 ) ) ;
#5281=VECTOR ( 'NONE', #20, 1000.000000000000114 ) ;
#5314=CARTESIAN_POINT ( 'NONE',  ( 2.339468227445713477, 3.268109542640643905, -2.700000000000003286 ) ) ;
#5332=ORIENTED_EDGE ( 'NONE', *, *, #6688, .F. ) ;
#5339=ADVANCED_FACE ( 'NONE', ( #3130 ), #3800, .F. ) ;
#5348=ORIENTED_EDGE ( 'NONE', *, *, #3930, .T. ) ;
#5365=CARTESIAN_POINT ( 'NONE',  ( 4.000000000000003553, 1.557668341133516154, -2.540303434304242547 ) ) ;
#5366=CARTESIAN_POINT ( 'NONE',  ( 0.000000000000000000, 0.000000000000000000, 0.000000000000000000 ) ) ;
#5380=DIRECTION ( 'NONE',  ( 1.000000000000000000, 0.000000000000000000, 0.000000000000000000 ) ) ;
#5381=CARTESIAN_POINT ( 'NONE',  ( -1.660531772554312724, 3.660093687634849324, 2.664342135588401717E-15 ) ) ;
#5384=FACE_OUTER_BOUND ( 'NONE', #3863, .T. ) ;
#5388=DIRECTION ( 'NONE',  ( 1.000000000000000000, 0.000000000000000000, 0.000000000000000000 ) ) ;
#5414=FACE_OUTER_BOUND ( 'NONE', #5140, .T. ) ;
#5421=CARTESIAN_POINT ( 'NONE',  ( -4.000000000000000000, 2.309401076758531346, -2.342734410091827701 ) ) ;
#5429=ORIENTED_EDGE ( 'NONE', *, *, #752, .F. ) ;
#5432=DIRECTION ( 'NONE',  ( -1.000000000000000000, 0.000000000000000000, 0.000000000000000000 ) ) ;
#5446=ORIENTED_EDGE ( 'NONE', *, *, #2430, .T. ) ;
#5461=B_SPLINE_CURVE_WITH_KNOTS ( 'NONE', 3,
 ( #6403, #4540, #5167, #2012, #7064, #3917 ),
 .UNSPECIFIED., .F., .F.,
 ( 4, 2, 4 ),
 ( 0.004120275011746843581, 0.005288420935197119671, 0.006456566858647395761 ),
 .UNSPECIFIED. ) ;
#5477=DIRECTION ( 'NONE',  ( 0.000000000000000000, -0.000000000000000000, 1.000000000000000000 ) ) ;
#5486=ORIENTED_EDGE ( 'NONE', *, *, #7922, .F. ) ;
#5497=CARTESIAN_POINT ( 'NONE',  ( 0.000000000000000000, 0.000000000000000000, -2.700000000000001066 ) ) ;
#5501=( GEOMETRIC_REPRESENTATION_CONTEXT ( 3 ) GLOBAL_UNCERTAINTY_ASSIGNED_CONTEXT ( ( #7792 ) ) GLOBAL_UNIT_ASSIGNED_CONTEXT ( ( #6154, #6780, #6734 ) ) REPRESENTATION_CONTEXT ( 'NONE', 'WORKASPACE' ) );
#5510=DIRECTION ( 'NONE',  ( -0.000000000000000000, 0.000000000000000000, -1.000000000000000000 ) ) ;
#5512=PRODUCT ( 'hex thin nut chamfered gradeab_iso_ISO - 4035 - M5 - N', 'hex thin nut chamfered gradeab_iso_ISO - 4035 - M5 - N', '', ( #7185 ) ) ;
#5520=CARTESIAN_POINT ( 'NONE',  ( 0.000000000000000000, 0.000000000000000000, 0.000000000000000000 ) ) ;
#5523=EDGE_CURVE ( 'NONE', #397, #6761, #6607, .T. ) ;
#5524=VERTEX_POINT ( 'NONE', #2085 ) ;
#5525=CARTESIAN_POINT ( 'NONE',  ( 1.660531772554324048, -3.660093687634887516, -2.070868501094675553E-14 ) ) ;
#5533=VERTEX_POINT ( 'NONE', #4731 ) ;
#5539=DIRECTION ( 'NONE',  ( -1.000000000000000000, 8.881784197001252323E-16, 0.000000000000000000 ) ) ;
#5546=AXIS2_PLACEMENT_3D ( 'NONE', #3670, #2332, #4165 ) ;
#5551=CIRCLE ( 'NONE', #2504, 2.099999999999999645 ) ;
#5568=EDGE_LOOP ( 'NONE', ( #3497, #349, #4217 ) ) ;
#5570=CARTESIAN_POINT ( 'NONE',  ( -4.000000000000000000, 0.7862748000878179155, -2.665527722372434738 ) ) ;
#5573=FACE_OUTER_BOUND ( 'NONE', #4055, .T. ) ;
#5591=FACE_OUTER_BOUND ( 'NONE', #6763, .T. ) ;
#5596=EDGE_CURVE ( 'NONE', #366, #4852, #6180, .T. ) ;
#5600=B_SPLINE_CURVE_WITH_KNOTS ( 'NONE', 3,
 ( #2845, #2176, #2882, #4023 ),
 .UNSPECIFIED., .F., .F.,
 ( 4, 4 ),
 ( 2.380737581608157039E-07, 0.002336974151641575941 ),
 .UNSPECIFIED. ) ;
#5601=ORIENTED_EDGE ( 'NONE', *, *, #1898, .T. ) ;
#5607=DIRECTION ( 'NONE',  ( -0.000000000000000000, -0.000000000000000000, 1.000000000000000000 ) ) ;
#5647=CARTESIAN_POINT ( 'NONE',  ( 0.000000000000000000, 0.000000000000000000, 0.000000000000000000 ) ) ;
#5649=CARTESIAN_POINT ( 'NONE',  ( 0.000000000000000000, 0.000000000000000000, 3.469446951953614189E-15 ) ) ;
#5653=CARTESIAN_POINT ( 'NONE',  ( -2.681483223904239210, 3.070647092368425923, 2.403443949632593102E-15 ) ) ;
#5656=CARTESIAN_POINT ( 'NONE',  ( -4.000000000000000000, -1.549102112939103160, -0.1578953385959410982 ) ) ;
#5679=LINE ( 'NONE', #3268, #5281 ) ;
#5683=EDGE_LOOP ( 'NONE', ( #3795, #2333, #7809 ) ) ;
#5684=CARTESIAN_POINT ( 'NONE',  ( 4.000000000000003553, -0.7779732554280840429, -0.03354435108168055818 ) ) ;
#5690=CARTESIAN_POINT ( 'NONE',  ( 1.214306433183764966E-14, 4.618802153517020059, 0.000000000000000000 ) ) ;
#5694=CARTESIAN_POINT ( 'NONE',  ( 0.000000000000000000, 0.000000000000000000, -0.3080913168122707546 ) ) ;
#5705=ORIENTED_EDGE ( 'NONE', *, *, #2432, .T. ) ;
#5709=AXIS2_PLACEMENT_3D ( 'NONE', #5520, #1199, #6265 ) ;
#5730=VECTOR ( 'NONE', #7862, 1000.000000000000000 ) ;
#5757=EDGE_LOOP ( 'NONE', ( #4398, #6437, #3955 ) ) ;
#5761=EDGE_CURVE ( 'NONE', #7226, #6726, #3810, .T. ) ;
#5780=FACE_OUTER_BOUND ( 'NONE', #2077, .T. ) ;
#5800=EDGE_CURVE ( 'NONE', #3286, #5533, #6975, .T. ) ;
#5844=AXIS2_PLACEMENT_3D ( 'NONE', #850, #2620, #6544 ) ;
#5847=AXIS2_PLACEMENT_3D ( 'NONE', #7489, #7527, #1894 ) ;
#5858=ORIENTED_EDGE ( 'NONE', *, *, #4261, .T. ) ;
#5874=AXIS2_PLACEMENT_3D ( 'NONE', #7202, #7328, #2720 ) ;
#5879=DIRECTION ( 'NONE',  ( 1.000000000000000000, 0.000000000000000000, 0.000000000000000000 ) ) ;
#5891=( LENGTH_UNIT ( ) NAMED_UNIT ( * ) SI_UNIT ( .MILLI., .METRE. ) );
#5893=ORIENTED_EDGE ( 'NONE', *, *, #5910, .T. ) ;
#5905=ORIENTED_EDGE ( 'NONE', *, *, #3443, .F. ) ;
#5910=EDGE_CURVE ( 'NONE', #3614, #3337, #131, .T. ) ;
#5913=DIRECTION ( 'NONE',  ( 0.000000000000000000, 0.000000000000000000, -1.000000000000000000 ) ) ;
#5917=CARTESIAN_POINT ( 'NONE',  ( -2.000000000000022649, -3.464101615137742396, 0.000000000000000000 ) ) ;
#5922=CARTESIAN_POINT ( 'NONE',  ( 2.678494666091051801, 3.072372537026354156, -2.665789719053470730 ) ) ;
#5923=FACE_OUTER_BOUND ( 'NONE', #3798, .T. ) ;
#5925=SURFACE_STYLE_USAGE ( .BOTH. , #1379 ) ;
#5928=B_SPLINE_CURVE_WITH_KNOTS ( 'NONE', 3,
 ( #969, #3427, #2214, #5917 ),
 .UNSPECIFIED., .F., .F.,
 ( 4, 4 ),
 ( 2.380737582494095533E-07, 0.002336974151641604998 ),
 .UNSPECIFIED. ) ;
#5933=ORIENTED_EDGE ( 'NONE', *, *, #5523, .F. ) ;
#5937=ADVANCED_FACE ( 'NONE', ( #7174 ), #1033, .T. ) ;
#5938=DIRECTION ( 'NONE',  ( 0.000000000000000000, 0.000000000000000000, 1.000000000000000000 ) ) ;
#5946=FACE_OUTER_BOUND ( 'NONE', #6020, .T. ) ;
#6014=CARTESIAN_POINT ( 'NONE',  ( 4.000000000000004441, 0.7862748000878159171, -2.665527722372431629 ) ) ;
#6020=EDGE_LOOP ( 'NONE', ( #2280, #6471, #3536 ) ) ;
#6021=ORIENTED_EDGE ( 'NONE', *, *, #3809, .F. ) ;
#6022=ORIENTED_EDGE ( 'NONE', *, *, #2075, .T. ) ;
#6028=CARTESIAN_POINT ( 'NONE',  ( -4.000000000000000000, -2.309401076758525573, -2.700000000000000178 ) ) ;
#6041=CARTESIAN_POINT ( 'NONE',  ( 0.000000000000000000, 0.000000000000000000, -2.700000000000001066 ) ) ;
#6047=ORIENTED_EDGE ( 'NONE', *, *, #1556, .F. ) ;
#6064=ORIENTED_EDGE ( 'NONE', *, *, #3219, .T. ) ;
#6094=CARTESIAN_POINT ( 'NONE',  ( 1.155036213957052500E-14, 4.618802153517020059, -2.700000000000000178 ) ) ;
#6099=EDGE_CURVE ( 'NONE', #3165, #2846, #7458, .T. ) ;
#6107=CONICAL_SURFACE ( 'NONE', #3997, 4.000000000000000000, 1.047197551196595855 ) ;
#6110=AXIS2_PLACEMENT_3D ( 'NONE', #5647, #6880, #3645 ) ;
#6119=ORIENTED_EDGE ( 'NONE', *, *, #6508, .T. ) ;
#6133=CARTESIAN_POINT ( 'NONE',  ( -3.673643420401911275, -2.497823135841289677, -0.2484800633750113841 ) ) ;
#6135=DIRECTION ( 'NONE',  ( -0.000000000000000000, -0.000000000000000000, 1.000000000000000000 ) ) ;
#6154=( LENGTH_UNIT ( ) NAMED_UNIT ( * ) SI_UNIT ( .MILLI., .METRE. ) );
#6171=CARTESIAN_POINT ( 'NONE',  ( 0.000000000000000000, 0.000000000000000000, -2.394516984716111185 ) ) ;
#6180=LINE ( 'NONE', #7435, #4506 ) ;
#6187=ORIENTED_EDGE ( 'NONE', *, *, #2430, .F. ) ;
#6193=CARTESIAN_POINT ( 'NONE',  ( 0.000000000000000000, 0.000000000000000000, -2.700000000000000178 ) ) ;
#6216=AXIS2_PLACEMENT_3D ( 'NONE', #5694, #6354, #6891 ) ;
#6221=ORIENTED_EDGE ( 'NONE', *, *, #4261, .F. ) ;
#6223=AXIS2_PLACEMENT_3D ( 'NONE', #5497, #6777, #995 ) ;
#6226=CARTESIAN_POINT ( 'NONE',  ( 3.345653888883671545, -2.687187980154741140, -2.560849780464844905 ) ) ;
#6227=CARTESIAN_POINT ( 'NONE',  ( -2.500000000000002220, 0.000000000000000000, -2.674599999999998978 ) ) ;
#6241=CIRCLE ( 'NONE', #5847, 4.000000000000000888 ) ;
#6243=AXIS2_PLACEMENT_3D ( 'NONE', #4250, #414, #3712 ) ;
#6245=SURFACE_STYLE_FILL_AREA ( #1168 ) ;
#6248=ORIENTED_EDGE ( 'NONE', *, *, #220, .F. ) ;
#6265=DIRECTION ( 'NONE',  ( -1.000000000000000000, 0.000000000000000000, 0.000000000000000000 ) ) ;
#6279=EDGE_LOOP ( 'NONE', ( #5446, #6064, #1254, #1851 ) ) ;
#6288=EDGE_LOOP ( 'NONE', ( #2416, #4230 ) ) ;
#6308=FACE_OUTER_BOUND ( 'NONE', #4758, .T. ) ;
#6311=FACE_OUTER_BOUND ( 'NONE', #2501, .T. ) ;
#6321=CONICAL_SURFACE ( 'NONE', #8030, 2.500000000000002220, 0.9599310885968777018 ) ;
#6330=CIRCLE ( 'NONE', #2084, 3.999999999999999112 ) ;
#6336=DIRECTION ( 'NONE',  ( -0.000000000000000000, -0.000000000000000000, 1.000000000000000000 ) ) ;
#6341=CIRCLE ( 'NONE', #1306, 2.500000000000002220 ) ;
#6342=DIRECTION ( 'NONE',  ( -0.000000000000000000, 0.000000000000000000, -1.000000000000000000 ) ) ;
#6354=DIRECTION ( 'NONE',  ( -0.000000000000000000, -0.000000000000000000, 1.000000000000000000 ) ) ;
#6355=PLANE ( 'NONE',  #334 ) ;
#6357=AXIS2_PLACEMENT_3D ( 'NONE', #1348, #3882, #6984 ) ;
#6360=EDGE_CURVE ( 'NONE', #6761, #7783, #3224, .T. ) ;
#6377=ORIENTED_EDGE ( 'NONE', *, *, #2706, .F. ) ;
#6396=ORIENTED_EDGE ( 'NONE', *, *, #5227, .F. ) ;
#6403=CARTESIAN_POINT ( 'NONE',  ( -4.000000000000000000, -2.309401076758531346, -2.342734410091827701 ) ) ;
#6410=DIRECTION ( 'NONE',  ( -1.000000000000000000, 0.000000000000000000, 0.000000000000000000 ) ) ;
#6426=MECHANICAL_DESIGN_GEOMETRIC_PRESENTATION_REPRESENTATION('',(#8000),#5501);
#6437=ORIENTED_EDGE ( 'NONE', *, *, #752, .T. ) ;
#6454=DIRECTION ( 'NONE',  ( 1.000000000000000000, 0.000000000000000000, 0.000000000000000000 ) ) ;
#6468=VERTEX_POINT ( 'NONE', #6766 ) ;
#6469=VERTEX_POINT ( 'NONE', #1075 ) ;
#6471=ORIENTED_EDGE ( 'NONE', *, *, #2167, .T. ) ;
#6475=DIRECTION ( 'NONE',  ( -0.8191520442889896891, 1.003171929053522158E-16, 0.5735764363510490460 ) ) ;
#6494=AXIS2_PLACEMENT_3D ( 'NONE', #1781, #5607, #2442 ) ;
#6508=EDGE_CURVE ( 'NONE', #6596, #7269, #3023, .T. ) ;
#6513=ORIENTED_EDGE ( 'NONE', *, *, #4461, .F. ) ;
#6523=VERTEX_POINT ( 'NONE', #1881 ) ;
#6536=ADVANCED_FACE ( 'NONE', ( #6311 ), #7680, .F. ) ;
#6544=DIRECTION ( 'NONE',  ( 1.000000000000000000, 0.000000000000000000, 0.000000000000000000 ) ) ;
#6548=UNCERTAINTY_MEASURE_WITH_UNIT (LENGTH_MEASURE( 1.000000000000000082E-05 ), #2424, 'distance_accuracy_value', 'NONE');
#6552=CARTESIAN_POINT ( 'NONE',  ( 0.3263565795980698514, -4.430380094434307914, -2.451519936624962703 ) ) ;
#6556=ORIENTED_EDGE ( 'NONE', *, *, #7062, .T. ) ;
#6569=ADVANCED_FACE ( 'NONE', ( #5573 ), #3748, .F. ) ;
#6585=ORIENTED_EDGE ( 'NONE', *, *, #5910, .F. ) ;
#6589=VECTOR ( 'NONE', #7547, 1000.000000000000000 ) ;
#6590=DIRECTION ( 'NONE',  ( 0.000000000000000000, -0.000000000000000000, 1.000000000000000000 ) ) ;
#6596=VERTEX_POINT ( 'NONE', #1151 ) ;
#6607=CIRCLE ( 'NONE', #7405, 4.000000000000000888 ) ;
#6619=CARTESIAN_POINT ( 'NONE',  ( 4.000000000000000000, 0.000000000000000000, 0.000000000000000000 ) ) ;
#6653=B_SPLINE_CURVE_WITH_KNOTS ( 'NONE', 3,
 ( #535, #6226, #8094, #3117 ),
 .UNSPECIFIED., .F., .F.,
 ( 4, 4 ),
 ( 2.380737581783742469E-07, 0.002336974151641522165 ),
 .UNSPECIFIED. ) ;
#6654=VECTOR ( 'NONE', #7908, 1000.000000000000000 ) ;
#6659=CARTESIAN_POINT ( 'NONE',  ( -0.6554360035617884384, 4.240386000424038571, -0.1586754815284916187 ) ) ;
#6688=EDGE_CURVE ( 'NONE', #4663, #7783, #2507, .T. ) ;
#6715=AXIS2_PLACEMENT_3D ( 'NONE', #7245, #391, #218 ) ;
#6716=FACE_OUTER_BOUND ( 'NONE', #6784, .T. ) ;
#6720=CARTESIAN_POINT ( 'NONE',  ( -4.000000000000000000, 2.309401076758531346, -2.342734410091827701 ) ) ;
#6726=VERTEX_POINT ( 'NONE', #343 ) ;
#6734=( NAMED_UNIT ( * ) SI_UNIT ( $, .STERADIAN. ) SOLID_ANGLE_UNIT ( ) );
#6736=AXIS2_PLACEMENT_3D ( 'NONE', #25, #6342, #3314 ) ;
#6761=VERTEX_POINT ( 'NONE', #217 ) ;
#6763=EDGE_LOOP ( 'NONE', ( #1543, #7817, #5246 ) ) ;
#6764=ADVANCED_FACE ( 'NONE', ( #7332 ), #3434, .T. ) ;
#6766=CARTESIAN_POINT ( 'NONE',  ( -2.000000000000009770, 3.464101615137749057, 0.000000000000000000 ) ) ;
#6771=APPLICATION_CONTEXT ( 'automotive_design' ) ;
#6777=DIRECTION ( 'NONE',  ( -0.000000000000000000, -0.000000000000000000, 1.000000000000000000 ) ) ;
#6780=( NAMED_UNIT ( * ) PLANE_ANGLE_UNIT ( ) SI_UNIT ( $, .RADIAN. ) );
#6781=ORIENTED_EDGE ( 'NONE', *, *, #4302, .F. ) ;
#6784=EDGE_LOOP ( 'NONE', ( #5705, #1686, #2586, #7150, #2579, #6377 ) ) ;
#6800=EDGE_CURVE ( 'NONE', #683, #366, #6341, .T. ) ;
#6824=ORIENTED_EDGE ( 'NONE', *, *, #6800, .F. ) ;
#6836=EDGE_CURVE ( 'NONE', #366, #683, #3419, .T. ) ;
#6837=CARTESIAN_POINT ( 'NONE',  ( 4.000000000000003553, 2.309401076758480720, -2.700000000000000178 ) ) ;
#6840=DIRECTION ( 'NONE',  ( -1.000000000000000000, 0.000000000000000000, 0.000000000000000000 ) ) ;
#6849=AXIS2_PLACEMENT_3D ( 'NONE', #4145, #2233, #4770 ) ;
#6880=DIRECTION ( 'NONE',  ( 0.000000000000000000, 0.000000000000000000, -1.000000000000000000 ) ) ;
#6887=ORIENTED_EDGE ( 'NONE', *, *, #6936, .T. ) ;
#6891=DIRECTION ( 'NONE',  ( 1.000000000000000000, 0.000000000000000000, 0.000000000000000000 ) ) ;
#6910=FILL_AREA_STYLE_COLOUR ( '', #1788 ) ;
#6915=EDGE_CURVE ( 'NONE', #683, #7269, #4307, .T. ) ;
#6916=EDGE_CURVE ( 'NONE', #3364, #2129, #2294, .T. ) ;
#6927=FACE_OUTER_BOUND ( 'NONE', #5757, .T. ) ;
#6930=CIRCLE ( 'NONE', #7186, 2.099999999999999645 ) ;
#6936=EDGE_CURVE ( 'NONE', #6468, #3337, #2097, .T. ) ;
#6952=DIRECTION ( 'NONE',  ( -1.000000000000000000, 0.000000000000000000, 0.000000000000000000 ) ) ;
#6971=ORIENTED_EDGE ( 'NONE', *, *, #1500, .T. ) ;
#6975=B_SPLINE_CURVE_WITH_KNOTS ( 'NONE', 3,
 ( #3212, #7643, #2491, #5037, #1962, #7564 ),
 .UNSPECIFIED., .F., .F.,
 ( 4, 2, 4 ),
 ( 0.006456566858647395761, 0.007625406818786647362, 0.008794246778925899830 ),
 .UNSPECIFIED. ) ;
#6984=DIRECTION ( 'NONE',  ( 1.000000000000000000, 0.000000000000000000, 0.000000000000000000 ) ) ;
#7017=CARTESIAN_POINT ( 'NONE',  ( 2.000000000000027089, 3.464101615137739731, 0.000000000000000000 ) ) ;
#7018=ORIENTED_EDGE ( 'NONE', *, *, #187, .F. ) ;
#7027=VECTOR ( 'NONE', #396, 1000.000000000000000 ) ;
#7054=CARTESIAN_POINT ( 'NONE',  ( -3.345653888883672433, 2.687187980154694955, -0.1391502195351393689 ) ) ;
#7058=SURFACE_STYLE_FILL_AREA ( #1491 ) ;
#7062=EDGE_CURVE ( 'NONE', #3249, #397, #3580, .T. ) ;
#7064=CARTESIAN_POINT ( 'NONE',  ( -4.000000000000000000, -0.3902508023145542793, -2.700000000000001066 ) ) ;
#7073=AXIS2_PLACEMENT_3D ( 'NONE', #1480, #1602, #5879 ) ;
#7080=DIRECTION ( 'NONE',  ( -0.000000000000000000, -0.000000000000000000, 1.000000000000000000 ) ) ;
#7088=CARTESIAN_POINT ( 'NONE',  ( 0.000000000000000000, 0.000000000000000000, -2.674599999999998978 ) ) ;
#7101=CARTESIAN_POINT ( 'NONE',  ( -2.339468227445729465, -3.268109542640674547, -2.699999999999984190 ) ) ;
#7113=ORIENTED_EDGE ( 'NONE', *, *, #6915, .F. ) ;
#7121=ADVANCED_FACE ( 'NONE', ( #333 ), #4110, .T. ) ;
#7150=ORIENTED_EDGE ( 'NONE', *, *, #860, .F. ) ;
#7160=ADVANCED_FACE ( 'NONE', ( #1005 ), #248, .T. ) ;
#7166=CARTESIAN_POINT ( 'NONE',  ( -7.502679033599690683E-14, -4.618802153517020059, -2.342734410091827701 ) ) ;
#7170=ORIENTED_EDGE ( 'NONE', *, *, #860, .T. ) ;
#7171=FACE_OUTER_BOUND ( 'NONE', #2088, .T. ) ;
#7174=FACE_OUTER_BOUND ( 'NONE', #1380, .T. ) ;
#7185=PRODUCT_CONTEXT ( 'NONE', #6771, 'mechanical' ) ;
#7186=AXIS2_PLACEMENT_3D ( 'NONE', #2817, #7789, #3483 ) ;
#7196=DIRECTION ( 'NONE',  ( -1.000000000000000000, 0.000000000000000000, 0.000000000000000000 ) ) ;
#7202=CARTESIAN_POINT ( 'NONE',  ( 0.000000000000000000, 0.000000000000000000, -25.03750572909317285 ) ) ;
#7208=DIRECTION ( 'NONE',  ( 0.5000000000000067724, 0.8660254037844348218, -0.000000000000000000 ) ) ;
#7209=CARTESIAN_POINT ( 'NONE',  ( 0.000000000000000000, 0.000000000000000000, -2.700000000000001066 ) ) ;
#7212=CARTESIAN_POINT ( 'NONE',  ( 4.000000000000003553, 2.309401076758524685, -2.342734410091827701 ) ) ;
#7218=EDGE_CURVE ( 'NONE', #2129, #3553, #7944, .T. ) ;
#7220=ORIENTED_EDGE ( 'NONE', *, *, #1898, .F. ) ;
#7223=CARTESIAN_POINT ( 'NONE',  ( 0.000000000000000000, 0.000000000000000000, -2.700000000000000178 ) ) ;
#7226=VERTEX_POINT ( 'NONE', #2471 ) ;
#7232=ADVANCED_BREP_SHAPE_REPRESENTATION ( '', ( #4069, #1587 ), #2305 ) ;
#7235=CARTESIAN_POINT ( 'NONE',  ( -2.099999999999999645, 2.571758278209440478E-16, -0.2800830152838832965 ) ) ;
#7245=CARTESIAN_POINT ( 'NONE',  ( 0.000000000000000000, 0.000000000000000000, -2.674599999999998978 ) ) ;
#7255=ORIENTED_EDGE ( 'NONE', *, *, #2727, .T. ) ;
#7264=VECTOR ( 'NONE', #5250, 1000.000000000000114 ) ;
#7269=VERTEX_POINT ( 'NONE', #424 ) ;
#7288=STYLED_ITEM ( 'NONE', ( #5162 ), #4069 ) ;
#7293=PLANE ( 'NONE',  #7875 ) ;
#7303=ORIENTED_EDGE ( 'NONE', *, *, #7218, .F. ) ;
#7322=CARTESIAN_POINT ( 'NONE',  ( 4.000000000000000000, 0.000000000000000000, 0.000000000000000000 ) ) ;
#7326=DIRECTION ( 'NONE',  ( 0.000000000000000000, 0.000000000000000000, -1.000000000000000000 ) ) ;
#7328=DIRECTION ( 'NONE',  ( -0.000000000000000000, -0.000000000000000000, 1.000000000000000000 ) ) ;
#7332=FACE_OUTER_BOUND ( 'NONE', #7811, .T. ) ;
#7365=UNCERTAINTY_MEASURE_WITH_UNIT (LENGTH_MEASURE( 1.000000000000000082E-05 ), #5891, 'distance_accuracy_value', 'NONE');
#7371=CARTESIAN_POINT ( 'NONE',  ( -2.000000000000022649, -3.464101615137742396, -2.700000000000001066 ) ) ;
#7373=CARTESIAN_POINT ( 'NONE',  ( 0.000000000000000000, 0.000000000000000000, 0.000000000000000000 ) ) ;
#7383=CARTESIAN_POINT ( 'NONE',  ( 2.000000000000010658, -3.464101615137748169, 0.000000000000000000 ) ) ;
#7400=ORIENTED_EDGE ( 'NONE', *, *, #1521, .T. ) ;
#7405=AXIS2_PLACEMENT_3D ( 'NONE', #7223, #6590, #4614 ) ;
#7408=CARTESIAN_POINT ( 'NONE',  ( 0.000000000000000000, 0.000000000000000000, 0.000000000000000000 ) ) ;
#7415=CONICAL_SURFACE ( 'NONE', #6110, 4.000000000000000000, 1.047197551196595855 ) ;
#7418=AXIS2_PLACEMENT_3D ( 'NONE', #5649, #6135, #4350 ) ;
#7422=LINE ( 'NONE', #6837, #2533 ) ;
#7428=AXIS2_PLACEMENT_3D ( 'NONE', #3922, #6410, #1260 ) ;
#7435=CARTESIAN_POINT ( 'NONE',  ( 2.500000000000002220, 0.000000000000000000, -25.03750572909317285 ) ) ;
#7451=ORIENTED_EDGE ( 'NONE', *, *, #6099, .T. ) ;
#7458=B_SPLINE_CURVE_WITH_KNOTS ( 'NONE', 3,
 ( #1564, #1652, #1063, #432, #6133, #3558 ),
 .UNSPECIFIED., .F., .F.,
 ( 4, 2, 4 ),
 ( 0.002336974151641604998, 0.003500975885716476645, 0.004664977619791348291 ),
 .UNSPECIFIED. ) ;
#7467=FACE_OUTER_BOUND ( 'NONE', #3849, .T. ) ;
#7489=CARTESIAN_POINT ( 'NONE',  ( 0.000000000000000000, 0.000000000000000000, -2.700000000000000178 ) ) ;
#7497=DIRECTION ( 'NONE',  ( -1.000000000000000000, 0.000000000000000000, 0.000000000000000000 ) ) ;
#7514=CARTESIAN_POINT ( 'NONE',  ( 1.084202172485504434E-14, 4.618802153517020948, -2.342734410091827701 ) ) ;
#7515=EDGE_CURVE ( 'NONE', #3165, #3286, #3734, .T. ) ;
#7517=CARTESIAN_POINT ( 'NONE',  ( 2.000000000000010658, -3.464101615137748169, 0.000000000000000000 ) ) ;
#7524=ORIENTED_EDGE ( 'NONE', *, *, #3771, .T. ) ;
#7527=DIRECTION ( 'NONE',  ( 0.000000000000000000, -0.000000000000000000, 1.000000000000000000 ) ) ;
#7546=ORIENTED_EDGE ( 'NONE', *, *, #4393, .T. ) ;
#7547=DIRECTION ( 'NONE',  ( -0.000000000000000000, -0.000000000000000000, 1.000000000000000000 ) ) ;
#7555=PLANE ( 'NONE',  #4867 ) ;
#7564=CARTESIAN_POINT ( 'NONE',  ( -4.000000000000000000, 2.309401076758496263, -0.3572655899081631503 ) ) ;
#7575=ORIENTED_EDGE ( 'NONE', *, *, #505, .F. ) ;
#7608=CARTESIAN_POINT ( 'NONE',  ( -1.660531772554312280, 3.660093687634850212, -2.700000000000004174 ) ) ;
#7615=ORIENTED_EDGE ( 'NONE', *, *, #5149, .T. ) ;
#7630=APPLICATION_CONTEXT ( 'automotive_design' ) ;
#7636=ADVANCED_FACE ( 'NONE', ( #3131 ), #5173, .T. ) ;
#7643=CARTESIAN_POINT ( 'NONE',  ( -4.000000000000000000, 0.3904826640788008341, -1.524659305057739994E-17 ) ) ;
#7646=EDGE_LOOP ( 'NONE', ( #6887, #6585, #1608 ) ) ;
#7679=CARTESIAN_POINT ( 'NONE',  ( 1.214306433183764966E-14, 4.618802153517020059, -2.700000000000000178 ) ) ;
#7680=CONICAL_SURFACE ( 'NONE', #6216, 2.060000000000000941, 0.9599310885968777018 ) ;
#7683=( NAMED_UNIT ( * ) PLANE_ANGLE_UNIT ( ) SI_UNIT ( $, .RADIAN. ) );
#7699=COLOUR_RGB ( '', 0.08235294, 0.09019608, 0.10196078) ;
#7700=ORIENTED_EDGE ( 'NONE', *, *, #2801, .T. ) ;
#7706=CARTESIAN_POINT ( 'NONE',  ( 0.000000000000000000, 0.000000000000000000, -2.700000000000001066 ) ) ;
#7715=FACE_OUTER_BOUND ( 'NONE', #5268, .T. ) ;
#7726=CARTESIAN_POINT ( 'NONE',  ( -3.673643420401911719, -2.497823135841289677, -2.451519936624989349 ) ) ;
#7752=DIRECTION ( 'NONE',  ( 0.000000000000000000, 0.000000000000000000, -1.000000000000000000 ) ) ;
#7753=CARTESIAN_POINT ( 'NONE',  ( -7.502679033599690683E-14, -4.618802153517020059, -2.342734410091827701 ) ) ;
#7759=ORIENTED_EDGE ( 'NONE', *, *, #4064, .F. ) ;
#7767=ORIENTED_EDGE ( 'NONE', *, *, #5596, .F. ) ;
#7783=VERTEX_POINT ( 'NONE', #7212 ) ;
#7789=DIRECTION ( 'NONE',  ( -0.000000000000000000, -0.000000000000000000, 1.000000000000000000 ) ) ;
#7792=UNCERTAINTY_MEASURE_WITH_UNIT (LENGTH_MEASURE( 1.000000000000000082E-05 ), #6154, 'distance_accuracy_value', 'NONE');
#7809=ORIENTED_EDGE ( 'NONE', *, *, #187, .T. ) ;
#7811=EDGE_LOOP ( 'NONE', ( #7170, #5893, #2268, #6781, #5332, #3819 ) ) ;
#7812=CIRCLE ( 'NONE', #4243, 2.500000000000002220 ) ;
#7817=ORIENTED_EDGE ( 'NONE', *, *, #2612, .T. ) ;
#7823=CARTESIAN_POINT ( 'NONE',  ( 0.000000000000000000, 0.000000000000000000, -2.700000000000000178 ) ) ;
#7833=DIRECTION ( 'NONE',  ( 1.000000000000000000, 0.000000000000000000, 0.000000000000000000 ) ) ;
#7834=DIRECTION ( 'NONE',  ( -1.000000000000000000, 0.000000000000000000, 0.000000000000000000 ) ) ;
#7842=CARTESIAN_POINT ( 'NONE',  ( 1.660531772554324492, -3.660093687634889736, -2.699999999999979305 ) ) ;
#7852=ORIENTED_EDGE ( 'NONE', *, *, #6936, .F. ) ;
#7853=ORIENTED_EDGE ( 'NONE', *, *, #2727, .F. ) ;
#7862=DIRECTION ( 'NONE',  ( 0.000000000000000000, 0.000000000000000000, 1.000000000000000000 ) ) ;
#7866=DIRECTION ( 'NONE',  ( 0.8660254037844372643, 0.5000000000000026645, 0.000000000000000000 ) ) ;
#7875=AXIS2_PLACEMENT_3D ( 'NONE', #4099, #3389, #7866 ) ;
#7879=CARTESIAN_POINT ( 'NONE',  ( 2.000000000000010658, -3.464101615137748169, -2.700000000000001066 ) ) ;
#7893=CARTESIAN_POINT ( 'NONE',  ( -1.321505333908964186, 3.855830693249143071, -0.03421028094653202900 ) ) ;
#7908=DIRECTION ( 'NONE',  ( 0.000000000000000000, 0.000000000000000000, 1.000000000000000000 ) ) ;
#7916=CARTESIAN_POINT ( 'NONE',  ( 4.000000000000003553, -0.7779732554280839318, -2.666455648918319987 ) ) ;
#7922=EDGE_CURVE ( 'NONE', #2129, #3337, #1860, .T. ) ;
#7937=CARTESIAN_POINT ( 'NONE',  ( -0.3263565795980840067, 4.430380094434251959, -0.2484800633750075816 ) ) ;
#7938=DIRECTION ( 'NONE',  ( -1.000000000000000000, 0.000000000000000000, 0.000000000000000000 ) ) ;
#7944=CIRCLE ( 'NONE', #781, 3.999999999999999112 ) ;
#7983=CARTESIAN_POINT ( 'NONE',  ( 0.000000000000000000, 0.000000000000000000, 0.000000000000000000 ) ) ;
#7989=DIRECTION ( 'NONE',  ( -1.000000000000000000, 0.000000000000000000, 0.000000000000000000 ) ) ;
#8000=STYLED_ITEM ( 'NONE', ( #1720 ), #7232 ) ;
#8020=LINE ( 'NONE', #3592, #3945 ) ;
#8030=AXIS2_PLACEMENT_3D ( 'NONE', #1479, #4017, #7196 ) ;
#8056=SURFACE_SIDE_STYLE ('',( #6245 ) ) ;
#8071=ADVANCED_FACE ( 'NONE', ( #3824 ), #7415, .T. ) ;
#8084=DIRECTION ( 'NONE',  ( -0.000000000000000000, -0.000000000000000000, 1.000000000000000000 ) ) ;
#8094=CARTESIAN_POINT ( 'NONE',  ( 2.681483223904246316, -3.070647092368468112, -2.699999999999980194 ) ) ;
#8095=DIRECTION ( 'NONE',  ( -0.8191520442889896891, 0.000000000000000000, -0.5735764363510490460 ) ) ;
#8096=CARTESIAN_POINT ( 'NONE',  ( -4.000000000000000000, 2.309401076758531346, -2.342734410091827701 ) ) ;
#8110=CARTESIAN_POINT ( 'NONE',  ( 0.000000000000000000, 0.000000000000000000, 0.000000000000000000 ) ) ;
#8118=CIRCLE ( 'NONE', #2690, 2.500000000000000444 ) ;
#8121=VERTEX_POINT ( 'NONE', #7166 ) ;
#8146=ORIENTED_EDGE ( 'NONE', *, *, #4393, .F. ) ;
#8173=CIRCLE ( 'NONE', #6715, 2.500000000000002220 ) ;
#8201=CARTESIAN_POINT ( 'NONE',  ( 4.000000000000003553, -0.3902508023145563332, -1.980363030680554193E-15 ) ) ;
ENDSEC;
END-ISO-10303-21;
